ISO-10303-21;
HEADER;
FILE_DESCRIPTION (('STEP AP214'),
    '1' );
FILE_NAME ('pan head cross recess screw_iso_ISO 7045 - M5 x 25 - Z - 25N.step',
    '2026-10-24T13:33:06',
    ( '' ),
    ( '' ),
    'SwSTEP 2.0',
    'SolidWorks 2026',
    '' );
FILE_SCHEMA (( 'AUTOMOTIVE_DESIGN' ));
ENDSEC;

DATA;
#2=AXIS2_PLACEMENT_3D ( 'NONE', #1029, #14245, #1184 ) ;
#31=AXIS2_PLACEMENT_3D ( 'NONE', #13162, #68, #13234 ) ;
#49=DIRECTION ( 'NONE',  ( 1.000000000000000000, 0.000000000000000000, 0.000000000000000000 ) ) ;
#62=EDGE_CURVE ( 'NONE', #11600, #2281, #14003, .T. ) ;
#68=DIRECTION ( 'NONE',  ( 1.000000000000000000, 0.000000000000000000, 0.000000000000000000 ) ) ;
#78=PLANE ( 'NONE',  #3254 ) ;
#82=EDGE_CURVE ( 'NONE', #232, #4077, #12381, .T. ) ;
#95=CIRCLE ( 'NONE', #11951, 2.700000000000000178 ) ;
#98=ORIENTED_EDGE ( 'NONE', *, *, #4977, .T. ) ;
#106=DIRECTION ( 'NONE',  ( 0.4461977533473793778, 0.8949343913984707521, -1.884057886186824495E-16 ) ) ;
#115=ORIENTED_EDGE ( 'NONE', *, *, #82, .F. ) ;
#117=CARTESIAN_POINT ( 'NONE',  ( 0.06760930072668894231, 0.9010842325122832008, -0.5150000000000000133 ) ) ;
#120=AXIS2_PLACEMENT_3D ( 'NONE', #1147, #9264, #49 ) ;
#131=DIRECTION ( 'NONE',  ( 0.4461977533474923430, -0.8949343913984144638, 0.000000000000000000 ) ) ;
#141=ADVANCED_FACE ( 'NONE', ( #13281 ), #9741, .F. ) ;
#142=AXIS2_PLACEMENT_3D ( 'NONE', #8631, #1337, #6858 ) ;
#146=CARTESIAN_POINT ( 'NONE',  ( 0.000000000000000000, -2.349999999999999201, 0.5149999999999992362 ) ) ;
#175=ORIENTED_EDGE ( 'NONE', *, *, #6775, .T. ) ;
#184=FACE_OUTER_BOUND ( 'NONE', #8422, .T. ) ;
#214=EDGE_CURVE ( 'NONE', #1600, #9602, #14242, .T. ) ;
#221=CARTESIAN_POINT ( 'NONE',  ( -25.39999999999996305, 0.000000000000000000, 0.000000000000000000 ) ) ;
#225=CARTESIAN_POINT ( 'NONE',  ( 8.000000000000000000, -4.837354856632045452E-15, -0.5150000000000000133 ) ) ;
#232=VERTEX_POINT ( 'NONE', #2038 ) ;
#242=ORIENTED_EDGE ( 'NONE', *, *, #12141, .F. ) ;
#246=VERTEX_POINT ( 'NONE', #11184 ) ;
#286=CARTESIAN_POINT ( 'NONE',  ( 2.740000000000000213, 0.5149999999999976819, 0.6774776749089244099 ) ) ;
#314=DIRECTION ( 'NONE',  ( -1.000000000000000000, -0.000000000000000000, -0.000000000000000000 ) ) ;
#333=ORIENTED_EDGE ( 'NONE', *, *, #6140, .F. ) ;
#334=CARTESIAN_POINT ( 'NONE',  ( 0.3226060873438392207, -0.5150000000000068967, 2.189154565102729766 ) ) ;
#339=EDGE_CURVE ( 'NONE', #9196, #8368, #11117, .T. ) ;
#348=LINE ( 'NONE', #12570, #6264 ) ;
#362=ADVANCED_FACE ( 'NONE', ( #8113 ), #12549, .T. ) ;
#371=EDGE_CURVE ( 'NONE', #10087, #1904, #448, .T. ) ;
#372=ORIENTED_EDGE ( 'NONE', *, *, #10389, .T. ) ;
#378=DIRECTION ( 'NONE',  ( 0.000000000000000000, 3.490239007934759657E-15, -1.000000000000000000 ) ) ;
#379=ORIENTED_EDGE ( 'NONE', *, *, #6538, .T. ) ;
#382=CARTESIAN_POINT ( 'NONE',  ( 2.740000000000000213, -0.5150000000000034550, 0.9838866223909983333 ) ) ;
#407=DIRECTION ( 'NONE',  ( -1.000000000000000000, -0.000000000000000000, -0.000000000000000000 ) ) ;
#418=AXIS2_PLACEMENT_3D ( 'NONE', #4704, #7151, #1554 ) ;
#421=DIRECTION ( 'NONE',  ( 0.8949343913984706411, -0.4461977533473793223, 7.082407382381129037E-17 ) ) ;
#437=ORIENTED_EDGE ( 'NONE', *, *, #7135, .F. ) ;
#448=B_SPLINE_CURVE_WITH_KNOTS ( 'NONE', 3,
 ( #117, #8932, #1150, #13343 ),
 .UNSPECIFIED., .F., .F.,
 ( 4, 4 ),
 ( 0.001586480563516618056, 0.004268227385920363680 ),
 .UNSPECIFIED. ) ;
#458=FACE_OUTER_BOUND ( 'NONE', #13462, .T. ) ;
#466=CARTESIAN_POINT ( 'NONE',  ( 0.06760930072668842883, -0.5149999999999961275, -0.9010842325122929708 ) ) ;
#472=ADVANCED_FACE ( 'NONE', ( #7101 ), #8920, .F. ) ;
#500=PRODUCT_DEFINITION_FORMATION_WITH_SPECIFIED_SOURCE ( 'ANY', '', #10165, .NOT_KNOWN. ) ;
#510=CARTESIAN_POINT ( 'NONE',  ( -25.39999999999996305, 0.000000000000000000, 2.500000000000000000 ) ) ;
#517=EDGE_CURVE ( 'NONE', #10395, #2635, #95, .T. ) ;
#529=ADVANCED_FACE ( 'NONE', ( #4940 ), #3828, .F. ) ;
#550=CARTESIAN_POINT ( 'NONE',  ( 7.345657149124340535, -9.419606183588304946E-15, 1.312408941150045472 ) ) ;
#551=AXIS2_PLACEMENT_3D ( 'NONE', #694, #9431, #11675 ) ;
#578=CARTESIAN_POINT ( 'NONE',  ( 0.000000000000000000, -0.5150000000000080069, 2.349999999999998312 ) ) ;
#587=AXIS2_PLACEMENT_3D ( 'NONE', #14240, #5547, #9979 ) ;
#661=DIRECTION ( 'NONE',  ( 0.000000000000000000, 1.000000000000000000, 3.280956645156627724E-15 ) ) ;
#669=AXIS2_PLACEMENT_3D ( 'NONE', #13246, #4259, #10035 ) ;
#688=DIRECTION ( 'NONE',  ( 0.000000000000000000, -1.000000000000000000, 0.000000000000000000 ) ) ;
#694=CARTESIAN_POINT ( 'NONE',  ( 2.740000000000000213, 0.000000000000000000, 0.000000000000000000 ) ) ;
#726=ORIENTED_EDGE ( 'NONE', *, *, #8107, .T. ) ;
#772=EDGE_LOOP ( 'NONE', ( #14040, #14210, #372, #7897 ) ) ;
#786=CARTESIAN_POINT ( 'NONE',  ( 0.000000000000000000, 0.5150000000000083400, -2.349999999999997424 ) ) ;
#790=PLANE ( 'NONE',  #910 ) ;
#793=CARTESIAN_POINT ( 'NONE',  ( -25.39999999999996305, 3.061616997868383141E-16, -2.500000000000000000 ) ) ;
#809=ORIENTED_EDGE ( 'NONE', *, *, #13309, .T. ) ;
#847=ORIENTED_EDGE ( 'NONE', *, *, #3069, .T. ) ;
#854=LINE ( 'NONE', #5313, #7831 ) ;
#870=LINE ( 'NONE', #2049, #4107 ) ;
#875=ORIENTED_EDGE ( 'NONE', *, *, #339, .F. ) ;
#880=ORIENTED_EDGE ( 'NONE', *, *, #8701, .F. ) ;
#883=CARTESIAN_POINT ( 'NONE',  ( 0.3226060873438262311, -0.5149999999999915756, -2.189154565102686245 ) ) ;
#910=AXIS2_PLACEMENT_3D ( 'NONE', #6337, #9380, #9456 ) ;
#914=CARTESIAN_POINT ( 'NONE',  ( 2.740000000000000213, -0.5149999999999961275, -0.9838866223905694541 ) ) ;
#919=ADVANCED_FACE ( 'NONE', ( #12596 ), #11585, .T. ) ;
#927=ORIENTED_EDGE ( 'NONE', *, *, #5351, .F. ) ;
#934=CARTESIAN_POINT ( 'NONE',  ( 2.740000000000000213, 0.9838866223909998876, -0.5150000000000000133 ) ) ;
#937=B_SPLINE_CURVE_WITH_KNOTS ( 'NONE', 3,
 ( #2803, #953, #11940, #10924 ),
 .UNSPECIFIED., .F., .F.,
 ( 4, 4 ),
 ( 0.001586480565025038831, 0.004268227387428736967 ),
 .UNSPECIFIED. ) ;
#953=CARTESIAN_POINT ( 'NONE',  ( 0.9586399445693637444, -0.8293189044373081575, 0.5149999999999994582 ) ) ;
#957=CARTESIAN_POINT ( 'NONE',  ( 0.06760930072668894231, -0.9010842325122859764, 0.5149999999999992362 ) ) ;
#963=AXIS2_PLACEMENT_3D ( 'NONE', #1507, #5945, #4658 ) ;
#972=EDGE_CURVE ( 'NONE', #11786, #6378, #9409, .T. ) ;
#988=ORIENTED_EDGE ( 'NONE', *, *, #82, .T. ) ;
#1011=DIRECTION ( 'NONE',  ( -0.3090169943749412895, 1.164708318489094811E-16, -0.9510565162951555296 ) ) ;
#1022=FACE_OUTER_BOUND ( 'NONE', #3384, .T. ) ;
#1024=LINE ( 'NONE', #146, #12894 ) ;
#1029=CARTESIAN_POINT ( 'NONE',  ( 8.000000000000000000, -4.896755294805453861E-15, 0.5150000000000000133 ) ) ;
#1031=DIRECTION ( 'NONE',  ( -1.000000000000000000, -0.000000000000000000, -0.000000000000000000 ) ) ;
#1036=CARTESIAN_POINT ( 'NONE',  ( 2.740000000000000213, -0.5150000000000034550, 0.9838866223909985553 ) ) ;
#1040=AXIS2_PLACEMENT_3D ( 'NONE', #7041, #3924, #2625 ) ;
#1058=ORIENTED_EDGE ( 'NONE', *, *, #8177, .F. ) ;
#1059=ORIENTED_EDGE ( 'NONE', *, *, #4977, .F. ) ;
#1076=ORIENTED_EDGE ( 'NONE', *, *, #6538, .F. ) ;
#1093=B_SPLINE_CURVE_WITH_KNOTS ( 'NONE', 3,
 ( #5901, #4967, #2642, #286 ),
 .UNSPECIFIED., .F., .F.,
 ( 4, 4 ),
 ( 0.001586480563516616538, 0.004268227385920363680 ),
 .UNSPECIFIED. ) ;
#1094=AXIS2_PLACEMENT_3D ( 'NONE', #7522, #1790, #13978 ) ;
#1098=VERTEX_POINT ( 'NONE', #6363 ) ;
#1102=CARTESIAN_POINT ( 'NONE',  ( 2.740000000000000213, 0.5150000000000035660, -0.9838866223905657904 ) ) ;
#1103=VERTEX_POINT ( 'NONE', #7658 ) ;
#1112=AXIS2_PLACEMENT_3D ( 'NONE', #2555, #4882, #5958 ) ;
#1129=EDGE_CURVE ( 'NONE', #4266, #2405, #348, .T. ) ;
#1147=CARTESIAN_POINT ( 'NONE',  ( 0.000000000000000000, 0.5149999999999917977, 2.350000000000000089 ) ) ;
#1150=CARTESIAN_POINT ( 'NONE',  ( 1.849560077140141257, 0.7556913915602415655, -0.5150000000000000133 ) ) ;
#1163=DIRECTION ( 'NONE',  ( 1.007709689656716938E-16, 1.000000000000000000, 3.606821995490528048E-15 ) ) ;
#1177=EDGE_CURVE ( 'NONE', #7747, #14235, #6647, .T. ) ;
#1184=DIRECTION ( 'NONE',  ( 0.000000000000000000, 1.000000000000000000, 1.086455722314322026E-16 ) ) ;
#1219=B_SPLINE_CURVE_WITH_KNOTS ( 'NONE', 3,
 ( #7556, #4084, #14301, #9750 ),
 .UNSPECIFIED., .F., .F.,
 ( 4, 4 ),
 ( 0.004656695504653254707, 0.007337072591785142629 ),
 .UNSPECIFIED. ) ;
#1225=CARTESIAN_POINT ( 'NONE',  ( 0.000000000000000000, 0.5149999999999917977, 2.350000000000000089 ) ) ;
#1251=ADVANCED_FACE ( 'NONE', ( #14005, #5249 ), #790, .F. ) ;
#1255=CARTESIAN_POINT ( 'NONE',  ( 0.06760930072668842883, -0.5149999999999961275, -0.9010842325122929708 ) ) ;
#1259=AXIS2_PLACEMENT_3D ( 'NONE', #225, #6483, #4453 ) ;
#1272=EDGE_LOOP ( 'NONE', ( #1972, #8916, #242, #11309, #9922 ) ) ;
#1305=CONICAL_SURFACE ( 'NONE', #9430, 0.8509999999999999787, 0.06981317007976602096 ) ;
#1337=DIRECTION ( 'NONE',  ( 1.007709689656716815E-16, 1.000000000000000000, 3.606821995490527259E-15 ) ) ;
#1344=EDGE_LOOP ( 'NONE', ( #12384, #12486, #11903, #8733 ) ) ;
#1358=DIRECTION ( 'NONE',  ( -1.000000000000000000, -0.000000000000000000, -0.000000000000000000 ) ) ;
#1387=VERTEX_POINT ( 'NONE', #9600 ) ;
#1399=EDGE_CURVE ( 'NONE', #11692, #1387, #14170, .T. ) ;
#1405=DIRECTION ( 'NONE',  ( -1.000000000000000000, -0.000000000000000000, -0.000000000000000000 ) ) ;
#1430=DIRECTION ( 'NONE',  ( 0.8949343913984143528, -1.557891129246500526E-15, 0.4461977533474922875 ) ) ;
#1432=DIRECTION ( 'NONE',  ( 0.000000000000000000, 1.000000000000000000, 1.086455722314322026E-16 ) ) ;
#1474=CARTESIAN_POINT ( 'NONE',  ( 3.900000000000000799, 0.000000000000000000, 0.000000000000000000 ) ) ;
#1507=CARTESIAN_POINT ( 'NONE',  ( 3.700000000000000178, 0.000000000000000000, 0.000000000000000000 ) ) ;
#1514=VERTEX_POINT ( 'NONE', #3077 ) ;
#1515=CARTESIAN_POINT ( 'NONE',  ( 2.740000000000000213, -0.9838866223905676778, 0.5149999999999995692 ) ) ;
#1538=VECTOR ( 'NONE', #2570, 1000.000000000000000 ) ;
#1540=AXIS2_PLACEMENT_3D ( 'NONE', #8940, #1163, #13353 ) ;
#1554=DIRECTION ( 'NONE',  ( 1.000000000000000000, 0.000000000000000000, 0.000000000000000000 ) ) ;
#1559=AXIS2_PLACEMENT_3D ( 'NONE', #9022, #11654, #13798 ) ;
#1572=ORIENTED_EDGE ( 'NONE', *, *, #3032, .F. ) ;
#1598=ORIENTED_EDGE ( 'NONE', *, *, #5147, .T. ) ;
#1600=VERTEX_POINT ( 'NONE', #7966 ) ;
#1619=ORIENTED_EDGE ( 'NONE', *, *, #4025, .T. ) ;
#1630=DIRECTION ( 'NONE',  ( -1.000000000000000000, 0.000000000000000000, -0.000000000000000000 ) ) ;
#1639=ORIENTED_EDGE ( 'NONE', *, *, #4832, .T. ) ;
#1645=( NAMED_UNIT ( * ) PLANE_ANGLE_UNIT ( ) SI_UNIT ( $, .RADIAN. ) );
#1652=( GEOMETRIC_REPRESENTATION_CONTEXT ( 3 ) GLOBAL_UNCERTAINTY_ASSIGNED_CONTEXT ( ( #11030 ) ) GLOBAL_UNIT_ASSIGNED_CONTEXT ( ( #8033, #5002, #8247 ) ) REPRESENTATION_CONTEXT ( 'NONE', 'WORKASPACE' ) );
#1697=EDGE_CURVE ( 'NONE', #2635, #10395, #4703, .T. ) ;
#1699=CARTESIAN_POINT ( 'NONE',  ( 0.3226060873438244547, -2.189154565102686245, -0.5150000000000000133 ) ) ;
#1720=AXIS2_PLACEMENT_3D ( 'NONE', #786, #10830, #13001 ) ;
#1726=DIRECTION ( 'NONE',  ( 0.000000000000000000, 0.000000000000000000, 1.000000000000000000 ) ) ;
#1782=EDGE_CURVE ( 'NONE', #13211, #246, #5177, .T. ) ;
#1790=DIRECTION ( 'NONE',  ( 0.000000000000000000, -1.000000000000000000, 0.000000000000000000 ) ) ;
#1791=ADVANCED_FACE ( 'NONE', ( #11678 ), #8406, .T. ) ;
#1829=LINE ( 'NONE', #793, #10825 ) ;
#1833=LINE ( 'NONE', #578, #3409 ) ;
#1837=PLANE ( 'NONE',  #4145 ) ;
#1840=CIRCLE ( 'NONE', #3596, 0.8509999999999999787 ) ;
#1859=ORIENTED_EDGE ( 'NONE', *, *, #5608, .F. ) ;
#1896=VERTEX_POINT ( 'NONE', #14270 ) ;
#1901=CARTESIAN_POINT ( 'NONE',  ( 1.794155980045911036, 0.000000000000000000, 0.000000000000000000 ) ) ;
#1904=VERTEX_POINT ( 'NONE', #5305 ) ;
#1905=DIRECTION ( 'NONE',  ( -0.3090169943749412895, 0.000000000000000000, 0.9510565162951555296 ) ) ;
#1914=CARTESIAN_POINT ( 'NONE',  ( 2.740000000000000213, 0.9838866223910001096, -0.5150000000000001243 ) ) ;
#1915=CIRCLE ( 'NONE', #2620, 0.2000000000000000944 ) ;
#1916=ORIENTED_EDGE ( 'NONE', *, *, #4025, .F. ) ;
#1932=ORIENTED_EDGE ( 'NONE', *, *, #10342, .F. ) ;
#1956=CARTESIAN_POINT ( 'NONE',  ( 7.345657149124969365, -5.313980200056029618E-16, -1.312408941149200148 ) ) ;
#1972=ORIENTED_EDGE ( 'NONE', *, *, #8819, .T. ) ;
#1977=DIRECTION ( 'NONE',  ( 1.000000000000000000, 0.000000000000000000, 0.000000000000000000 ) ) ;
#2031=CARTESIAN_POINT ( 'NONE',  ( 2.740000000000000213, -0.5150000000000022338, 0.6774776749089210792 ) ) ;
#2038=CARTESIAN_POINT ( 'NONE',  ( 3.699999999999998401, 0.000000000000000000, 4.750000000000000000 ) ) ;
#2049=CARTESIAN_POINT ( 'NONE',  ( 2.740000000000000213, -0.9838866223905674557, -0.5150000000000000133 ) ) ;
#2058=AXIS2_PLACEMENT_3D ( 'NONE', #7166, #13910, #8326 ) ;
#2102=DIRECTION ( 'NONE',  ( 0.4461977533474923430, -0.8949343913984144638, 0.000000000000000000 ) ) ;
#2104=CARTESIAN_POINT ( 'NONE',  ( 1.849560077140107950, -0.5150000000000023448, 0.7556913915602430087 ) ) ;
#2114=APPLICATION_CONTEXT ( 'automotive_design' ) ;
#2119=EDGE_LOOP ( 'NONE', ( #5406, #333, #1859, #7797 ) ) ;
#2123=CARTESIAN_POINT ( 'NONE',  ( 0.3074992278157512304, 2.196686566159293807, -2.407412430484044816E-32 ) ) ;
#2132=ORIENTED_EDGE ( 'NONE', *, *, #371, .T. ) ;
#2135=PLANE ( 'NONE',  #31 ) ;
#2155=AXIS2_PLACEMENT_3D ( 'NONE', #8596, #14171, #9980 ) ;
#2164=ADVANCED_FACE ( 'NONE', ( #11580 ), #12881, .T. ) ;
#2175=UNCERTAINTY_MEASURE_WITH_UNIT (LENGTH_MEASURE( 1.000000000000000082E-05 ), #11453, 'distance_accuracy_value', 'NONE');
#2190=ORIENTED_EDGE ( 'NONE', *, *, #13328, .T. ) ;
#2209=CARTESIAN_POINT ( 'NONE',  ( 2.740000000000000213, 0.000000000000000000, 0.000000000000000000 ) ) ;
#2229=EDGE_CURVE ( 'NONE', #2405, #6772, #8897, .T. ) ;
#2238=ORIENTED_EDGE ( 'NONE', *, *, #13328, .F. ) ;
#2255=PLANE ( 'NONE',  #120 ) ;
#2275=SHAPE_REPRESENTATION ( 'pan head cross recess screw_iso_ISO 7045 - M5 x 25 - Z - 25N', ( #14039 ), #4225 ) ;
#2279=EDGE_CURVE ( 'NONE', #8841, #9866, #1840, .T. ) ;
#2281=VERTEX_POINT ( 'NONE', #10865 ) ;
#2287=AXIS2_PLACEMENT_3D ( 'NONE', #1914, #7279, #8436 ) ;
#2325=CARTESIAN_POINT ( 'NONE',  ( 8.000000000000000000, 0.5150000000000000133, 1.798112889504231112E-15 ) ) ;
#2326=EDGE_LOOP ( 'NONE', ( #10559, #6317, #1076, #2403 ) ) ;
#2337=CARTESIAN_POINT ( 'NONE',  ( 0.06760930072668812352, 0.5150000000000032330, -0.9010842325122888630 ) ) ;
#2403=ORIENTED_EDGE ( 'NONE', *, *, #2229, .T. ) ;
#2405=VERTEX_POINT ( 'NONE', #12584 ) ;
#2446=ORIENTED_EDGE ( 'NONE', *, *, #5628, .F. ) ;
#2447=EDGE_CURVE ( 'NONE', #6099, #11786, #4990, .T. ) ;
#2450=ORIENTED_EDGE ( 'NONE', *, *, #972, .T. ) ;
#2458=SHAPE_REPRESENTATION_RELATIONSHIP ( 'NONE' , 'NONE' ,  #2275, #6456 ) ;
#2480=CIRCLE ( 'NONE', #7799, 4.556291390728477886 ) ;
#2481=FACE_OUTER_BOUND ( 'NONE', #7158, .T. ) ;
#2504=CIRCLE ( 'NONE', #10359, 7.864440107515430434 ) ;
#2514=DIRECTION ( 'NONE',  ( 0.000000000000000000, -1.000000000000000000, -3.491481338843133355E-15 ) ) ;
#2515=DIRECTION ( 'NONE',  ( 0.8949343913984706411, 1.557891129246106293E-15, -0.4461977533473793778 ) ) ;
#2523=CIRCLE ( 'NONE', #2058, 2.500000000000000000 ) ;
#2526=ORIENTED_EDGE ( 'NONE', *, *, #10124, .T. ) ;
#2528=ORIENTED_EDGE ( 'NONE', *, *, #8434, .F. ) ;
#2539=ORIENTED_EDGE ( 'NONE', *, *, #10370, .F. ) ;
#2555=CARTESIAN_POINT ( 'NONE',  ( 2.740000000000000213, 0.000000000000000000, 0.000000000000000000 ) ) ;
#2564=CIRCLE ( 'NONE', #12753, 7.983406227920510467 ) ;
#2570=DIRECTION ( 'NONE',  ( 0.000000000000000000, -1.000000000000000000, -1.652937667529658626E-16 ) ) ;
#2579=ORIENTED_EDGE ( 'NONE', *, *, #5198, .T. ) ;
#2580=CIRCLE ( 'NONE', #2, 7.983406227920510467 ) ;
#2586=ORIENTED_EDGE ( 'NONE', *, *, #11382, .F. ) ;
#2610=CIRCLE ( 'NONE', #12329, 7.983406227920510467 ) ;
#2614=AXIS2_PLACEMENT_3D ( 'NONE', #12834, #5163, #1726 ) ;
#2620=AXIS2_PLACEMENT_3D ( 'NONE', #3379, #8948, #7642 ) ;
#2621=EDGE_CURVE ( 'NONE', #1904, #8368, #3907, .T. ) ;
#2625=DIRECTION ( 'NONE',  ( 0.000000000000000000, -3.552713678800500929E-15, -1.000000000000000000 ) ) ;
#2630=DIRECTION ( 'NONE',  ( 0.000000000000000000, 0.000000000000000000, 1.000000000000000000 ) ) ;
#2635=VERTEX_POINT ( 'NONE', #13638 ) ;
#2642=CARTESIAN_POINT ( 'NONE',  ( 1.849560077140140812, 0.5149999999999973488, 0.7556913915602433418 ) ) ;
#2644=CYLINDRICAL_SURFACE ( 'NONE', #8833, 4.749999999999999112 ) ;
#2666=DIRECTION ( 'NONE',  ( 0.000000000000000000, 0.000000000000000000, 1.000000000000000000 ) ) ;
#2686=ADVANCED_FACE ( 'NONE', ( #2481 ), #12625, .T. ) ;
#2722=ORIENTED_EDGE ( 'NONE', *, *, #4726, .T. ) ;
#2736=PLANE ( 'NONE',  #418 ) ;
#2748=CARTESIAN_POINT ( 'NONE',  ( 3.900000000000000799, 0.000000000000000000, 2.700000000000000178 ) ) ;
#2754=DIRECTION ( 'NONE',  ( -1.000000000000000000, -0.000000000000000000, -0.000000000000000000 ) ) ;
#2763=CARTESIAN_POINT ( 'NONE',  ( 0.06760930072668894231, 0.9010842325122760954, 0.5149999999999993472 ) ) ;
#2803=CARTESIAN_POINT ( 'NONE',  ( 0.06760930072668894231, -0.9010842325122859764, 0.5149999999999992362 ) ) ;
#2804=( NAMED_UNIT ( * ) SI_UNIT ( $, .STERADIAN. ) SOLID_ANGLE_UNIT ( ) );
#2821=MECHANICAL_DESIGN_GEOMETRIC_PRESENTATION_REPRESENTATION('',(#8373),#1652);
#2870=EDGE_CURVE ( 'NONE', #8841, #8377, #854, .T. ) ;
#2959=EDGE_CURVE ( 'NONE', #5706, #1098, #4613, .T. ) ;
#2985=CARTESIAN_POINT ( 'NONE',  ( 0.000000000000000000, -2.349999999999997424, 0.5149999999999992362 ) ) ;
#2987=CARTESIAN_POINT ( 'NONE',  ( 0.000000000000000000, -2.349999999999997424, 0.5149999999999992362 ) ) ;
#3022=CIRCLE ( 'NONE', #10422, 8.000000000000000000 ) ;
#3032=EDGE_CURVE ( 'NONE', #9866, #7620, #9007, .T. ) ;
#3037=CIRCLE ( 'NONE', #13897, 0.2000000000000000944 ) ;
#3059=ORIENTED_EDGE ( 'NONE', *, *, #10660, .F. ) ;
#3069=EDGE_CURVE ( 'NONE', #5337, #9188, #2564, .T. ) ;
#3077=CARTESIAN_POINT ( 'NONE',  ( 2.740000000000000213, 1.042174426074397490E-16, -0.8509999999999999787 ) ) ;
#3100=ORIENTED_EDGE ( 'NONE', *, *, #5991, .T. ) ;
#3126=CYLINDRICAL_SURFACE ( 'NONE', #4688, 2.500000000000000000 ) ;
#3131=ADVANCED_FACE ( 'NONE', ( #184 ), #12297, .F. ) ;
#3139=ADVANCED_FACE ( 'NONE', ( #13690 ), #3955, .F. ) ;
#3146=CARTESIAN_POINT ( 'NONE',  ( 3.699999999999998401, 0.000000000000000000, 0.000000000000000000 ) ) ;
#3152=EDGE_CURVE ( 'NONE', #6825, #4266, #12067, .T. ) ;
#3160=DIRECTION ( 'NONE',  ( 0.000000000000000000, 0.000000000000000000, 1.000000000000000000 ) ) ;
#3161=DIRECTION ( 'NONE',  ( 0.000000000000000000, 0.000000000000000000, 1.000000000000000000 ) ) ;
#3169=DIRECTION ( 'NONE',  ( 0.000000000000000000, 0.000000000000000000, 1.000000000000000000 ) ) ;
#3172=CIRCLE ( 'NONE', #3621, 0.8509999999999999787 ) ;
#3176=CARTESIAN_POINT ( 'NONE',  ( 3.699999999999998401, 0.000000000000000000, 0.000000000000000000 ) ) ;
#3190=CARTESIAN_POINT ( 'NONE',  ( 2.740000000000000213, -0.6774776749089230776, 0.5149999999999995692 ) ) ;
#3204=ORIENTED_EDGE ( 'NONE', *, *, #13931, .T. ) ;
#3205=DIRECTION ( 'NONE',  ( 0.000000000000000000, 1.000000000000000000, 1.153406566473941260E-16 ) ) ;
#3212=CARTESIAN_POINT ( 'NONE',  ( 0.06760930072668813740, -0.5150000000000026779, 0.9010842325122891960 ) ) ;
#3213=CARTESIAN_POINT ( 'NONE',  ( 0.3074992278157369086, -2.196686566159251619, -2.690165171976911629E-16 ) ) ;
#3233=EDGE_CURVE ( 'NONE', #2635, #5030, #3037, .T. ) ;
#3254=AXIS2_PLACEMENT_3D ( 'NONE', #12020, #6643, #4539 ) ;
#3272=AXIS2_PLACEMENT_3D ( 'NONE', #4333, #11883, #5357 ) ;
#3278=DIRECTION ( 'NONE',  ( 0.4461977533473793778, -2.936240938438015166E-15, 0.8949343913984707521 ) ) ;
#3315=DIRECTION ( 'NONE',  ( -1.000000000000000000, -0.000000000000000000, -0.000000000000000000 ) ) ;
#3324=DIRECTION ( 'NONE',  ( 0.000000000000000000, -2.105246936865057050E-16, -1.000000000000000000 ) ) ;
#3379=CARTESIAN_POINT ( 'NONE',  ( 3.900000000000000799, 3.306546357697853733E-16, -2.700000000000000178 ) ) ;
#3384=EDGE_LOOP ( 'NONE', ( #10536, #12548 ) ) ;
#3388=DIRECTION ( 'NONE',  ( 0.000000000000000000, 0.000000000000000000, 1.000000000000000000 ) ) ;
#3409=VECTOR ( 'NONE', #6262, 1000.000000000000114 ) ;
#3441=DIRECTION ( 'NONE',  ( 0.8949343913984143528, 0.4461977533474922875, 0.000000000000000000 ) ) ;
#3443=CIRCLE ( 'NONE', #1094, 0.4499999999999985678 ) ;
#3465=PLANE ( 'NONE',  #142 ) ;
#3472=AXIS2_PLACEMENT_3D ( 'NONE', #9114, #5849, #8381 ) ;
#3489=CIRCLE ( 'NONE', #4155, 4.556291390728477886 ) ;
#3492=ORIENTED_EDGE ( 'NONE', *, *, #12141, .T. ) ;
#3522=DIRECTION ( 'NONE',  ( 0.000000000000000000, 0.000000000000000000, 1.000000000000000000 ) ) ;
#3549=ORIENTED_EDGE ( 'NONE', *, *, #9332, .F. ) ;
#3578=CARTESIAN_POINT ( 'NONE',  ( 2.740000000000000213, 0.000000000000000000, 0.000000000000000000 ) ) ;
#3580=EDGE_CURVE ( 'NONE', #8981, #1904, #7440, .T. ) ;
#3589=CLOSED_SHELL ( 'NONE', ( #3131, #10392, #8160, #2686, #1791, #919, #12214, #8081, #4643, #12876, #7286, #10456, #5274, #5350, #362, #12962, #6089, #5007, #11103, #1251, #9468, #9610, #10646, #10107, #4962, #3751, #2164, #9040, #141, #12685, #3139, #529, #472, #11366 ) ) ;
#3596=AXIS2_PLACEMENT_3D ( 'NONE', #13092, #6434, #8824 ) ;
#3621=AXIS2_PLACEMENT_3D ( 'NONE', #13336, #5587, #14283 ) ;
#3625=ORIENTED_EDGE ( 'NONE', *, *, #9490, .T. ) ;
#3636=DIRECTION ( 'NONE',  ( 0.000000000000000000, -2.664535259100375697E-15, -1.000000000000000000 ) ) ;
#3655=DIRECTION ( 'NONE',  ( 0.000000000000000000, 1.000000000000000000, 0.000000000000000000 ) ) ;
#3665=DIRECTION ( 'NONE',  ( 0.000000000000000000, 0.000000000000000000, 1.000000000000000000 ) ) ;
#3678=FACE_OUTER_BOUND ( 'NONE', #7255, .T. ) ;
#3738=CARTESIAN_POINT ( 'NONE',  ( 1.794155980045911036, 5.817072295949926440E-16, -4.749999999999999112 ) ) ;
#3740=LINE ( 'NONE', #8153, #12568 ) ;
#3747=DIRECTION ( 'NONE',  ( -0.000000000000000000, 1.000000000000000000, 1.224646799147353207E-16 ) ) ;
#3751=ADVANCED_FACE ( 'NONE', ( #10098 ), #13426, .F. ) ;
#3768=FILL_AREA_STYLE_COLOUR ( '', #10709 ) ;
#3786=CARTESIAN_POINT ( 'NONE',  ( 2.740000000000000213, 0.5150000000000024558, -0.6774776749089207462 ) ) ;
#3789=SHAPE_DEFINITION_REPRESENTATION ( #9119, #2275 ) ;
#3820=EDGE_LOOP ( 'NONE', ( #3204, #2586, #4776, #4282 ) ) ;
#3825=DIRECTION ( 'NONE',  ( -1.000000000000000000, -0.000000000000000000, -0.000000000000000000 ) ) ;
#3828=CONICAL_SURFACE ( 'NONE', #10086, 0.8509999999999999787, 0.06981317007976602096 ) ;
#3838=CARTESIAN_POINT ( 'NONE',  ( 2.740000000000000213, 0.000000000000000000, 0.000000000000000000 ) ) ;
#3845=CARTESIAN_POINT ( 'NONE',  ( 0.9586399445693646326, 0.8293189044373081575, 0.5149999999999996803 ) ) ;
#3850=DIRECTION ( 'NONE',  ( 0.000000000000000000, -1.000000000000000000, -1.652937667529658626E-16 ) ) ;
#3851=AXIS2_PLACEMENT_3D ( 'NONE', #2987, #13120, #3205 ) ;
#3862=EDGE_CURVE ( 'NONE', #4077, #11692, #9149, .T. ) ;
#3894=CARTESIAN_POINT ( 'NONE',  ( 0.3226060873438383325, 0.5149999999999923528, 2.189154565102733319 ) ) ;
#3898=ORIENTED_EDGE ( 'NONE', *, *, #6140, .T. ) ;
#3906=CARTESIAN_POINT ( 'NONE',  ( 0.000000000000000000, 0.5150000000000083400, -2.349999999999997424 ) ) ;
#3907=CIRCLE ( 'NONE', #1112, 0.8509999999999999787 ) ;
#3917=EDGE_LOOP ( 'NONE', ( #4509, #10710, #10725, #9876 ) ) ;
#3924=DIRECTION ( 'NONE',  ( -1.000000000000000000, -0.000000000000000000, -0.000000000000000000 ) ) ;
#3934=EDGE_LOOP ( 'NONE', ( #115, #6026 ) ) ;
#3955=CONICAL_SURFACE ( 'NONE', #8589, 0.8509999999999999787, 0.06981317007976602096 ) ;
#3977=EDGE_CURVE ( 'NONE', #7393, #1896, #3489, .T. ) ;
#4016=ORIENTED_EDGE ( 'NONE', *, *, #3152, .F. ) ;
#4025=EDGE_CURVE ( 'NONE', #9866, #5706, #6230, .T. ) ;
#4043=ORIENTED_EDGE ( 'NONE', *, *, #1782, .F. ) ;
#4064=ORIENTED_EDGE ( 'NONE', *, *, #3032, .T. ) ;
#4073=CARTESIAN_POINT ( 'NONE',  ( 2.740000000000000213, 0.000000000000000000, 0.8509999999999999787 ) ) ;
#4077=VERTEX_POINT ( 'NONE', #5382 ) ;
#4084=CARTESIAN_POINT ( 'NONE',  ( 1.849560077140141257, -0.7556913915602415655, -0.5150000000000000133 ) ) ;
#4089=DIRECTION ( 'NONE',  ( -1.000000000000000000, -0.000000000000000000, -0.000000000000000000 ) ) ;
#4107=VECTOR ( 'NONE', #7632, 1000.000000000000000 ) ;
#4139=DIRECTION ( 'NONE',  ( 1.007709689656716815E-16, 1.153406566473941260E-16, -1.000000000000000000 ) ) ;
#4145=AXIS2_PLACEMENT_3D ( 'NONE', #13802, #8215, #12723 ) ;
#4153=ORIENTED_EDGE ( 'NONE', *, *, #1697, .F. ) ;
#4154=DIRECTION ( 'NONE',  ( -1.000000000000000000, -0.000000000000000000, -0.000000000000000000 ) ) ;
#4155=AXIS2_PLACEMENT_3D ( 'NONE', #13129, #8855, #14216 ) ;
#4177=PLANE ( 'NONE',  #6085 ) ;
#4180=ORIENTED_EDGE ( 'NONE', *, *, #1697, .T. ) ;
#4184=CARTESIAN_POINT ( 'NONE',  ( 0.000000000000000000, 2.350000000000000089, -0.5150000000000000133 ) ) ;
#4206=DIRECTION ( 'NONE',  ( 0.000000000000000000, 0.000000000000000000, 1.000000000000000000 ) ) ;
#4213=LINE ( 'NONE', #13252, #8272 ) ;
#4225=( GEOMETRIC_REPRESENTATION_CONTEXT ( 3 ) GLOBAL_UNCERTAINTY_ASSIGNED_CONTEXT ( ( #2175 ) ) GLOBAL_UNIT_ASSIGNED_CONTEXT ( ( #11453, #1645, #6084 ) ) REPRESENTATION_CONTEXT ( 'NONE', 'WORKASPACE' ) );
#4238=DIRECTION ( 'NONE',  ( 0.8949343913984144638, 0.4461977533474923430, 0.000000000000000000 ) ) ;
#4241=DIRECTION ( 'NONE',  ( -1.000000000000000000, -0.000000000000000000, -0.000000000000000000 ) ) ;
#4259=DIRECTION ( 'NONE',  ( 1.007709689656716815E-16, 1.000000000000000000, 3.606821995490527259E-15 ) ) ;
#4266=VERTEX_POINT ( 'NONE', #8467 ) ;
#4274=ORIENTED_EDGE ( 'NONE', *, *, #13487, .F. ) ;
#4277=EDGE_CURVE ( 'NONE', #5030, #11926, #2523, .T. ) ;
#4282=ORIENTED_EDGE ( 'NONE', *, *, #371, .F. ) ;
#4313=ORIENTED_EDGE ( 'NONE', *, *, #2959, .T. ) ;
#4333=CARTESIAN_POINT ( 'NONE',  ( -996.9834933385058093, 0.000000000000000000, 0.000000000000000000 ) ) ;
#4336=ORIENTED_EDGE ( 'NONE', *, *, #12038, .T. ) ;
#4362=CARTESIAN_POINT ( 'NONE',  ( 7.345657149124338758, 1.312408941150044583, 0.000000000000000000 ) ) ;
#4397=ORIENTED_EDGE ( 'NONE', *, *, #5628, .T. ) ;
#4399=DIRECTION ( 'NONE',  ( 0.000000000000000000, -1.000000000000000000, -3.702006032529638986E-15 ) ) ;
#4453=DIRECTION ( 'NONE',  ( 1.000000000000000000, 0.000000000000000000, 0.000000000000000000 ) ) ;
#4500=CARTESIAN_POINT ( 'NONE',  ( 1.424271237134740131, 0.000000000000000000, 4.556291390728477886 ) ) ;
#4509=ORIENTED_EDGE ( 'NONE', *, *, #3862, .F. ) ;
#4530=DIRECTION ( 'NONE',  ( 1.000000000000000000, 0.000000000000000000, 0.000000000000000000 ) ) ;
#4539=DIRECTION ( 'NONE',  ( -0.8949343913984706411, 0.4461977533473793223, 0.000000000000000000 ) ) ;
#4545=CARTESIAN_POINT ( 'NONE',  ( 8.000000000000000000, -4.837354856632045452E-15, -0.5150000000000000133 ) ) ;
#4574=DIRECTION ( 'NONE',  ( -1.000000000000000000, -0.000000000000000000, -0.000000000000000000 ) ) ;
#4613=CIRCLE ( 'NONE', #7503, 0.8509999999999999787 ) ;
#4615=EDGE_CURVE ( 'NONE', #11692, #13924, #12270, .T. ) ;
#4632=EDGE_LOOP ( 'NONE', ( #2526, #927, #7833, #10777 ) ) ;
#4643=ADVANCED_FACE ( 'NONE', ( #3678 ), #2736, .T. ) ;
#4658=DIRECTION ( 'NONE',  ( 0.000000000000000000, 0.000000000000000000, 1.000000000000000000 ) ) ;
#4669=LINE ( 'NONE', #5675, #10599 ) ;
#4670=ORIENTED_EDGE ( 'NONE', *, *, #5608, .T. ) ;
#4683=DIRECTION ( 'NONE',  ( -1.000000000000000000, -0.000000000000000000, -0.000000000000000000 ) ) ;
#4688=AXIS2_PLACEMENT_3D ( 'NONE', #10810, #9724, #14127 ) ;
#4703=CIRCLE ( 'NONE', #963, 2.700000000000000178 ) ;
#4704=CARTESIAN_POINT ( 'NONE',  ( 0.000000000000000000, 2.349999999999998312, -0.5150000000000000133 ) ) ;
#4710=DIRECTION ( 'NONE',  ( 0.000000000000000000, 0.000000000000000000, 1.000000000000000000 ) ) ;
#4726=EDGE_CURVE ( 'NONE', #7747, #9211, #6710, .T. ) ;
#4728=VERTEX_POINT ( 'NONE', #3894 ) ;
#4754=DIRECTION ( 'NONE',  ( 0.000000000000000000, 0.000000000000000000, 1.000000000000000000 ) ) ;
#4760=DIRECTION ( 'NONE',  ( 0.000000000000000000, 3.490239007934759657E-15, -1.000000000000000000 ) ) ;
#4773=ORIENTED_EDGE ( 'NONE', *, *, #2959, .F. ) ;
#4776=ORIENTED_EDGE ( 'NONE', *, *, #2621, .F. ) ;
#4787=CIRCLE ( 'NONE', #9919, 4.749999999999999112 ) ;
#4790=EDGE_LOOP ( 'NONE', ( #12382, #8039, #7229, #6257, #5294 ) ) ;
#4832=EDGE_CURVE ( 'NONE', #1103, #6772, #11874, .T. ) ;
#4838=ORIENTED_EDGE ( 'NONE', *, *, #7993, .T. ) ;
#4843=ORIENTED_EDGE ( 'NONE', *, *, #8449, .T. ) ;
#4844=FACE_OUTER_BOUND ( 'NONE', #4632, .T. ) ;
#4862=SURFACE_STYLE_USAGE ( .BOTH. , #10362 ) ;
#4867=CARTESIAN_POINT ( 'NONE',  ( 3.700000000000000178, 0.000000000000000000, 0.000000000000000000 ) ) ;
#4875=ORIENTED_EDGE ( 'NONE', *, *, #6775, .F. ) ;
#4882=DIRECTION ( 'NONE',  ( -1.000000000000000000, -0.000000000000000000, -0.000000000000000000 ) ) ;
#4911=CARTESIAN_POINT ( 'NONE',  ( 2.740000000000000213, 0.000000000000000000, 0.000000000000000000 ) ) ;
#4940=FACE_OUTER_BOUND ( 'NONE', #3820, .T. ) ;
#4962=ADVANCED_FACE ( 'NONE', ( #6432 ), #78, .F. ) ;
#4967=CARTESIAN_POINT ( 'NONE',  ( 0.9586399445693768451, 0.5149999999999971267, 0.8293189044373084906 ) ) ;
#4971=CARTESIAN_POINT ( 'NONE',  ( 2.740000000000000213, -0.5150000000000034550, 0.9838866223909985553 ) ) ;
#4977=EDGE_CURVE ( 'NONE', #9188, #7620, #8321, .T. ) ;
#4985=EDGE_CURVE ( 'NONE', #1896, #6825, #3022, .T. ) ;
#4990=CIRCLE ( 'NONE', #1259, 7.983406227920510467 ) ;
#5002=( NAMED_UNIT ( * ) PLANE_ANGLE_UNIT ( ) SI_UNIT ( $, .RADIAN. ) );
#5007=ADVANCED_FACE ( 'NONE', ( #8823 ), #9985, .T. ) ;
#5030=VERTEX_POINT ( 'NONE', #13307 ) ;
#5039=CARTESIAN_POINT ( 'NONE',  ( 3.016506661494197328, 0.000000000000000000, 7.007546303702493782E-17 ) ) ;
#5055=EDGE_CURVE ( 'NONE', #4077, #232, #13884, .T. ) ;
#5059=DIRECTION ( 'NONE',  ( -1.000000000000000000, -0.000000000000000000, -0.000000000000000000 ) ) ;
#5063=CIRCLE ( 'NONE', #1559, 7.983406227920510467 ) ;
#5073=DIRECTION ( 'NONE',  ( 0.000000000000000000, 1.000000000000000000, 0.000000000000000000 ) ) ;
#5077=DIRECTION ( 'NONE',  ( 1.000000000000000000, 0.000000000000000000, 0.000000000000000000 ) ) ;
#5144=EDGE_LOOP ( 'NONE', ( #847, #8562, #12265, #12251 ) ) ;
#5147=EDGE_CURVE ( 'NONE', #13924, #1600, #7161, .T. ) ;
#5150=CARTESIAN_POINT ( 'NONE',  ( 2.740000000000000213, -0.5149999999999973488, -0.6774776749089248540 ) ) ;
#5152=DIRECTION ( 'NONE',  ( -1.000000000000000000, -0.000000000000000000, -0.000000000000000000 ) ) ;
#5163=DIRECTION ( 'NONE',  ( -1.000000000000000000, -0.000000000000000000, -0.000000000000000000 ) ) ;
#5177=CIRCLE ( 'NONE', #7011, 7.864440107515430434 ) ;
#5178=DIRECTION ( 'NONE',  ( -1.000000000000000000, -0.000000000000000000, -0.000000000000000000 ) ) ;
#5198=EDGE_CURVE ( 'NONE', #9987, #7747, #10956, .T. ) ;
#5249=FACE_OUTER_BOUND ( 'NONE', #3934, .T. ) ;
#5263=FACE_OUTER_BOUND ( 'NONE', #2326, .T. ) ;
#5274=ADVANCED_FACE ( 'NONE', ( #9542 ), #6266, .T. ) ;
#5293=AXIS2_PLACEMENT_3D ( 'NONE', #2985, #4139, #6239 ) ;
#5294=ORIENTED_EDGE ( 'NONE', *, *, #5147, .F. ) ;
#5305=CARTESIAN_POINT ( 'NONE',  ( 2.740000000000000213, 0.6774776749089226335, -0.5150000000000000133 ) ) ;
#5313=CARTESIAN_POINT ( 'NONE',  ( 2.740000000000000213, 0.9838866223910003317, 0.5149999999999999023 ) ) ;
#5323=ORIENTED_EDGE ( 'NONE', *, *, #11382, .T. ) ;
#5337=VERTEX_POINT ( 'NONE', #10479 ) ;
#5340=DIRECTION ( 'NONE',  ( -1.000000000000000000, 0.000000000000000000, -0.000000000000000000 ) ) ;
#5347=CARTESIAN_POINT ( 'NONE',  ( 0.06760930072668806801, -4.837354856632045452E-15, 0.000000000000000000 ) ) ;
#5350=ADVANCED_FACE ( 'NONE', ( #5263 ), #1837, .T. ) ;
#5351=EDGE_CURVE ( 'NONE', #11341, #5839, #10631, .T. ) ;
#5356=DIRECTION ( 'NONE',  ( 0.8949343913984143528, 0.4461977533474922875, 0.000000000000000000 ) ) ;
#5357=DIRECTION ( 'NONE',  ( 0.000000000000000000, 0.000000000000000000, 1.000000000000000000 ) ) ;
#5382=CARTESIAN_POINT ( 'NONE',  ( 3.699999999999998401, 5.817072295949927426E-16, -4.750000000000000000 ) ) ;
#5406=ORIENTED_EDGE ( 'NONE', *, *, #2870, .F. ) ;
#5416=DIRECTION ( 'NONE',  ( -1.000000000000000000, -0.000000000000000000, -0.000000000000000000 ) ) ;
#5433=ORIENTED_EDGE ( 'NONE', *, *, #2279, .T. ) ;
#5451=DIRECTION ( 'NONE',  ( -1.000000000000000000, -0.000000000000000000, -0.000000000000000000 ) ) ;
#5469=AXIS2_PLACEMENT_3D ( 'NONE', #11590, #3825, #2666 ) ;
#5486=DIRECTION ( 'NONE',  ( 0.000000000000000000, 3.656775105596099119E-15, -1.000000000000000000 ) ) ;
#5489=AXIS2_PLACEMENT_3D ( 'NONE', #8660, #9682, #1977 ) ;
#5547=DIRECTION ( 'NONE',  ( -1.000000000000000000, -0.000000000000000000, -0.000000000000000000 ) ) ;
#5558=AXIS2_PLACEMENT_3D ( 'NONE', #10328, #10189, #3665 ) ;
#5564=ORIENTED_EDGE ( 'NONE', *, *, #12357, .T. ) ;
#5587=DIRECTION ( 'NONE',  ( -1.000000000000000000, -0.000000000000000000, -0.000000000000000000 ) ) ;
#5608=EDGE_CURVE ( 'NONE', #6378, #9211, #4669, .T. ) ;
#5625=DIRECTION ( 'NONE',  ( -0.8949343913984706411, 0.4461977533473793223, 0.000000000000000000 ) ) ;
#5628=EDGE_CURVE ( 'NONE', #8368, #1514, #11302, .T. ) ;
#5660=DIRECTION ( 'NONE',  ( 0.000000000000000000, -1.000000000000000000, -3.491481338843133355E-15 ) ) ;
#5675=CARTESIAN_POINT ( 'NONE',  ( 2.740000000000000213, -0.9838866223905674557, -0.5150000000000000133 ) ) ;
#5682=DIRECTION ( 'NONE',  ( 0.8949343913984143528, 0.4461977533474921764, 1.416481476476136321E-16 ) ) ;
#5706=VERTEX_POINT ( 'NONE', #4073 ) ;
#5707=AXIS2_PLACEMENT_3D ( 'NONE', #7074, #13602, #13812 ) ;
#5755=LINE ( 'NONE', #12364, #1538 ) ;
#5770=FACE_OUTER_BOUND ( 'NONE', #14152, .T. ) ;
#5814=ORIENTED_EDGE ( 'NONE', *, *, #2447, .F. ) ;
#5828=DIRECTION ( 'NONE',  ( -0.000000000000000000, 0.000000000000000000, -1.000000000000000000 ) ) ;
#5839=VERTEX_POINT ( 'NONE', #9665 ) ;
#5849=DIRECTION ( 'NONE',  ( -1.000000000000000000, -0.000000000000000000, -0.000000000000000000 ) ) ;
#5860=ORIENTED_EDGE ( 'NONE', *, *, #214, .F. ) ;
#5869=FILL_AREA_STYLE ('',( #3768 ) ) ;
#5873=DIRECTION ( 'NONE',  ( 0.000000000000000000, -3.491481338843133355E-15, 1.000000000000000000 ) ) ;
#5878=ORIENTED_EDGE ( 'NONE', *, *, #6771, .T. ) ;
#5901=CARTESIAN_POINT ( 'NONE',  ( 0.06760930072668799862, 0.5149999999999969047, 0.9010842325122926377 ) ) ;
#5921=CARTESIAN_POINT ( 'NONE',  ( 0.06760930072668894231, -0.9010842325122929708, -0.5150000000000000133 ) ) ;
#5923=CARTESIAN_POINT ( 'NONE',  ( 8.000000000000000000, -4.837354856632045452E-15, 0.000000000000000000 ) ) ;
#5936=SURFACE_STYLE_FILL_AREA ( #5869 ) ;
#5941=EDGE_LOOP ( 'NONE', ( #6267, #11551, #3625, #11612 ) ) ;
#5942=ORIENTED_EDGE ( 'NONE', *, *, #1782, .T. ) ;
#5945=DIRECTION ( 'NONE',  ( -1.000000000000000000, -0.000000000000000000, -0.000000000000000000 ) ) ;
#5957=VECTOR ( 'NONE', #7764, 1000.000000000000000 ) ;
#5958=DIRECTION ( 'NONE',  ( 0.000000000000000000, 0.000000000000000000, 1.000000000000000000 ) ) ;
#5961=PRODUCT_CONTEXT ( 'NONE', #2114, 'mechanical' ) ;
#5980=VECTOR ( 'NONE', #1430, 1000.000000000000114 ) ;
#5991=EDGE_CURVE ( 'NONE', #4728, #11362, #7092, .T. ) ;
#6026=ORIENTED_EDGE ( 'NONE', *, *, #5055, .F. ) ;
#6040=DIRECTION ( 'NONE',  ( 0.000000000000000000, 0.000000000000000000, 1.000000000000000000 ) ) ;
#6071=DIRECTION ( 'NONE',  ( -0.000000000000000000, 0.000000000000000000, 1.000000000000000000 ) ) ;
#6075=TOROIDAL_SURFACE ( 'NONE', #9089, 2.700000000000000178, 0.2000000000000000111 ) ;
#6083=CARTESIAN_POINT ( 'NONE',  ( 2.740000000000000213, -0.9838866223905674557, -0.5150000000000000133 ) ) ;
#6084=( NAMED_UNIT ( * ) SI_UNIT ( $, .STERADIAN. ) SOLID_ANGLE_UNIT ( ) );
#6085=AXIS2_PLACEMENT_3D ( 'NONE', #7645, #5340, #8669 ) ;
#6089=ADVANCED_FACE ( 'NONE', ( #10021 ), #2255, .T. ) ;
#6099=VERTEX_POINT ( 'NONE', #5921 ) ;
#6111=CARTESIAN_POINT ( 'NONE',  ( 28.70000000000000284, 0.000000000000000000, 0.000000000000000000 ) ) ;
#6138=CARTESIAN_POINT ( 'NONE',  ( 2.740000000000000213, 0.9838866223910001096, -0.5150000000000001243 ) ) ;
#6140=EDGE_CURVE ( 'NONE', #9211, #8841, #3172, .T. ) ;
#6181=ORIENTED_EDGE ( 'NONE', *, *, #3069, .F. ) ;
#6189=UNCERTAINTY_MEASURE_WITH_UNIT (LENGTH_MEASURE( 1.000000000000000082E-05 ), #13673, 'distance_accuracy_value', 'NONE');
#6196=AXIS2_PLACEMENT_3D ( 'NONE', #1956, #3278, #7680 ) ;
#6225=CARTESIAN_POINT ( 'NONE',  ( 1.794155980045911036, 0.000000000000000000, 0.000000000000000000 ) ) ;
#6230=CIRCLE ( 'NONE', #13867, 0.8509999999999999787 ) ;
#6239=DIRECTION ( 'NONE',  ( 0.000000000000000000, 1.000000000000000000, 1.153406566473941260E-16 ) ) ;
#6240=EDGE_LOOP ( 'NONE', ( #3549, #4274, #12865, #437 ) ) ;
#6257=ORIENTED_EDGE ( 'NONE', *, *, #12593, .F. ) ;
#6262=DIRECTION ( 'NONE',  ( 0.8949343913984706411, 1.487067055422294855E-15, -0.4461977533473793223 ) ) ;
#6264=VECTOR ( 'NONE', #421, 1000.000000000000114 ) ;
#6266=PLANE ( 'NONE',  #2287 ) ;
#6267=ORIENTED_EDGE ( 'NONE', *, *, #12357, .F. ) ;
#6317=ORIENTED_EDGE ( 'NONE', *, *, #3580, .F. ) ;
#6337=CARTESIAN_POINT ( 'NONE',  ( 3.700000000000000178, 2.500000000000000000, 0.000000000000000000 ) ) ;
#6353=FACE_OUTER_BOUND ( 'NONE', #2119, .T. ) ;
#6358=DIRECTION ( 'NONE',  ( 0.8949343913984706411, -0.4461977533473793778, 0.000000000000000000 ) ) ;
#6363=CARTESIAN_POINT ( 'NONE',  ( 2.740000000000000213, 0.5149999999999976819, 0.6774776749089244099 ) ) ;
#6378=VERTEX_POINT ( 'NONE', #6083 ) ;
#6386=ORIENTED_EDGE ( 'NONE', *, *, #4985, .F. ) ;
#6399=DIRECTION ( 'NONE',  ( 0.000000000000000000, 0.000000000000000000, 1.000000000000000000 ) ) ;
#6424=LINE ( 'NONE', #1102, #7459 ) ;
#6432=FACE_OUTER_BOUND ( 'NONE', #10071, .T. ) ;
#6434=DIRECTION ( 'NONE',  ( -1.000000000000000000, -0.000000000000000000, -0.000000000000000000 ) ) ;
#6456=ADVANCED_BREP_SHAPE_REPRESENTATION ( '', ( #13134, #14039 ), #4225 ) ;
#6470=CARTESIAN_POINT ( 'NONE',  ( 8.000000000000000000, -4.837354856632045452E-15, 0.000000000000000000 ) ) ;
#6483=DIRECTION ( 'NONE',  ( -0.000000000000000000, 0.000000000000000000, 1.000000000000000000 ) ) ;
#6535=CARTESIAN_POINT ( 'NONE',  ( 1.794155980045909482, 0.000000000000000000, 0.000000000000000000 ) ) ;
#6538=EDGE_CURVE ( 'NONE', #2405, #8981, #5755, .T. ) ;
#6556=CARTESIAN_POINT ( 'NONE',  ( 2.740000000000000213, 0.5150000000000035660, -0.9838866223905657904 ) ) ;
#6571=CARTESIAN_POINT ( 'NONE',  ( 2.740000000000000213, -0.5150000000000034550, 0.9838866223909985553 ) ) ;
#6611=AXIS2_PLACEMENT_3D ( 'NONE', #1225, #5660, #10156 ) ;
#6620=PLANE ( 'NONE',  #5489 ) ;
#6638=DIRECTION ( 'NONE',  ( -1.000000000000000000, -0.000000000000000000, -0.000000000000000000 ) ) ;
#6643=DIRECTION ( 'NONE',  ( 0.4461977533473793778, 0.8949343913984707521, -1.884057886186824742E-16 ) ) ;
#6647=LINE ( 'NONE', #1036, #9275 ) ;
#6692=CARTESIAN_POINT ( 'NONE',  ( -25.39999999999996305, 0.000000000000000000, 4.749999999999999112 ) ) ;
#6702=ORIENTED_EDGE ( 'NONE', *, *, #8177, .T. ) ;
#6705=CARTESIAN_POINT ( 'NONE',  ( 3.900000000000000799, 0.000000000000000000, 0.000000000000000000 ) ) ;
#6710=CIRCLE ( 'NONE', #3472, 0.8509999999999999787 ) ;
#6770=ORIENTED_EDGE ( 'NONE', *, *, #12428, .T. ) ;
#6771=EDGE_CURVE ( 'NONE', #9211, #6099, #1219, .T. ) ;
#6772=VERTEX_POINT ( 'NONE', #934 ) ;
#6775=EDGE_CURVE ( 'NONE', #5337, #9602, #13547, .T. ) ;
#6792=ORIENTED_EDGE ( 'NONE', *, *, #7135, .T. ) ;
#6816=EDGE_CURVE ( 'NONE', #7102, #1514, #11995, .T. ) ;
#6825=VERTEX_POINT ( 'NONE', #2123 ) ;
#6858=DIRECTION ( 'NONE',  ( 0.000000000000000000, -3.606821995490527259E-15, 1.000000000000000000 ) ) ;
#6879=CARTESIAN_POINT ( 'NONE',  ( 8.000000000000000000, -4.896755294805453861E-15, 0.5150000000000000133 ) ) ;
#6890=ORIENTED_EDGE ( 'NONE', *, *, #12428, .F. ) ;
#6900=( GEOMETRIC_REPRESENTATION_CONTEXT ( 3 ) GLOBAL_UNCERTAINTY_ASSIGNED_CONTEXT ( ( #6189 ) ) GLOBAL_UNIT_ASSIGNED_CONTEXT ( ( #13673, #9399, #2804 ) ) REPRESENTATION_CONTEXT ( 'NONE', 'WORKASPACE' ) );
#6929=DIRECTION ( 'NONE',  ( 1.000000000000000000, 0.000000000000000000, 0.000000000000000000 ) ) ;
#6932=PLANE ( 'NONE',  #5707 ) ;
#6969=CARTESIAN_POINT ( 'NONE',  ( 1.849560077140108394, 0.7556913915602446741, 0.5149999999999996803 ) ) ;
#6974=CARTESIAN_POINT ( 'NONE',  ( -25.39999999999996305, 0.000000000000000000, 0.000000000000000000 ) ) ;
#7011=AXIS2_PLACEMENT_3D ( 'NONE', #550, #8186, #11753 ) ;
#7041=CARTESIAN_POINT ( 'NONE',  ( 0.06760930072668806801, -4.837354856632045452E-15, 0.000000000000000000 ) ) ;
#7044=ORIENTED_EDGE ( 'NONE', *, *, #13071, .F. ) ;
#7074=CARTESIAN_POINT ( 'NONE',  ( 2.740000000000000213, -0.5150000000000034550, 0.9838866223909985553 ) ) ;
#7092=CIRCLE ( 'NONE', #10574, 7.983406227920510467 ) ;
#7101=FACE_OUTER_BOUND ( 'NONE', #772, .T. ) ;
#7102=VERTEX_POINT ( 'NONE', #13706 ) ;
#7107=FACE_OUTER_BOUND ( 'NONE', #6240, .T. ) ;
#7117=DIRECTION ( 'NONE',  ( -1.000000000000000000, -0.000000000000000000, -0.000000000000000000 ) ) ;
#7135=EDGE_CURVE ( 'NONE', #8981, #8755, #7267, .T. ) ;
#7143=ORIENTED_EDGE ( 'NONE', *, *, #4985, .T. ) ;
#7151=DIRECTION ( 'NONE',  ( -0.000000000000000000, 0.000000000000000000, 1.000000000000000000 ) ) ;
#7158=EDGE_LOOP ( 'NONE', ( #988, #11180, #10482, #8479 ) ) ;
#7159=EDGE_CURVE ( 'NONE', #11362, #8755, #9412, .T. ) ;
#7161=CIRCLE ( 'NONE', #5558, 4.556291390728477886 ) ;
#7165=VECTOR ( 'NONE', #3324, 1000.000000000000000 ) ;
#7166=CARTESIAN_POINT ( 'NONE',  ( 3.900000000000000799, 0.000000000000000000, 0.000000000000000000 ) ) ;
#7169=DIRECTION ( 'NONE',  ( 0.000000000000000000, 0.000000000000000000, 1.000000000000000000 ) ) ;
#7229=ORIENTED_EDGE ( 'NONE', *, *, #8875, .T. ) ;
#7255=EDGE_LOOP ( 'NONE', ( #4670, #5878, #12645, #2450 ) ) ;
#7267=B_SPLINE_CURVE_WITH_KNOTS ( 'NONE', 3,
 ( #12693, #6969, #3845, #2763 ),
 .UNSPECIFIED., .F., .F.,
 ( 4, 4 ),
 ( 0.004656695506220394354, 0.007337072593346776264 ),
 .UNSPECIFIED. ) ;
#7279=DIRECTION ( 'NONE',  ( -1.000000000000000000, 0.000000000000000000, -0.000000000000000000 ) ) ;
#7286=ADVANCED_FACE ( 'NONE', ( #8480 ), #8700, .T. ) ;
#7393=VERTEX_POINT ( 'NONE', #4500 ) ;
#7426=LINE ( 'NONE', #6556, #11293 ) ;
#7435=ORIENTED_EDGE ( 'NONE', *, *, #517, .T. ) ;
#7440=CIRCLE ( 'NONE', #7885, 0.8509999999999999787 ) ;
#7445=AXIS2_PLACEMENT_3D ( 'NONE', #2209, #6638, #3522 ) ;
#7459=VECTOR ( 'NONE', #4399, 1000.000000000000000 ) ;
#7476=CIRCLE ( 'NONE', #2155, 1.037871761867652065 ) ;
#7497=CARTESIAN_POINT ( 'NONE',  ( 2.740000000000000213, 0.000000000000000000, 0.000000000000000000 ) ) ;
#7503=AXIS2_PLACEMENT_3D ( 'NONE', #8780, #9945, #12181 ) ;
#7504=EDGE_LOOP ( 'NONE', ( #13418, #2539, #880, #4043 ) ) ;
#7506=CARTESIAN_POINT ( 'NONE',  ( 3.900000000000000799, 0.000000000000000000, 0.000000000000000000 ) ) ;
#7517=AXIS2_PLACEMENT_3D ( 'NONE', #3146, #5451, #6399 ) ;
#7519=EDGE_CURVE ( 'NONE', #2281, #11600, #12647, .T. ) ;
#7522=CARTESIAN_POINT ( 'NONE',  ( 1.794155980045909482, 0.000000000000000000, 4.300000000000001599 ) ) ;
#7553=ORIENTED_EDGE ( 'NONE', *, *, #4832, .F. ) ;
#7556=CARTESIAN_POINT ( 'NONE',  ( 2.740000000000000213, -0.6774776749089226335, -0.5150000000000000133 ) ) ;
#7594=ORIENTED_EDGE ( 'NONE', *, *, #2229, .F. ) ;
#7610=CARTESIAN_POINT ( 'NONE',  ( 0.9586399445693629673, -0.5150000000000024558, 0.8293189044373063812 ) ) ;
#7620=VERTEX_POINT ( 'NONE', #12967 ) ;
#7629=AXIS2_PLACEMENT_3D ( 'NONE', #6974, #7117, #2630 ) ;
#7632=DIRECTION ( 'NONE',  ( 0.000000000000000000, 1.000000000000000000, 0.000000000000000000 ) ) ;
#7642=DIRECTION ( 'NONE',  ( 0.000000000000000000, -1.224646799147353207E-16, 1.000000000000000000 ) ) ;
#7645=CARTESIAN_POINT ( 'NONE',  ( 2.740000000000000213, 0.9838866223910001096, -0.5150000000000001243 ) ) ;
#7658=CARTESIAN_POINT ( 'NONE',  ( 0.3226060873438401089, 2.189154565102731098, -0.5150000000000000133 ) ) ;
#7680=DIRECTION ( 'NONE',  ( 0.8949343913984707521, 0.000000000000000000, -0.4461977533473793223 ) ) ;
#7693=DIRECTION ( 'NONE',  ( 0.000000000000000000, 0.000000000000000000, 1.000000000000000000 ) ) ;
#7741=ORIENTED_EDGE ( 'NONE', *, *, #9332, .T. ) ;
#7746=EDGE_LOOP ( 'NONE', ( #13920, #5323, #8770, #8354 ) ) ;
#7747=VERTEX_POINT ( 'NONE', #5150 ) ;
#7764=DIRECTION ( 'NONE',  ( -1.000000000000000000, -0.000000000000000000, -0.000000000000000000 ) ) ;
#7797=ORIENTED_EDGE ( 'NONE', *, *, #12675, .T. ) ;
#7799=AXIS2_PLACEMENT_3D ( 'NONE', #9820, #8936, #10090 ) ;
#7824=CARTESIAN_POINT ( 'NONE',  ( 2.740000000000000213, -0.5150000000000022338, 0.6774776749089210792 ) ) ;
#7829=ORIENTED_EDGE ( 'NONE', *, *, #214, .T. ) ;
#7831=VECTOR ( 'NONE', #3850, 1000.000000000000000 ) ;
#7833=ORIENTED_EDGE ( 'NONE', *, *, #7993, .F. ) ;
#7850=DIRECTION ( 'NONE',  ( 0.000000000000000000, 0.000000000000000000, 1.000000000000000000 ) ) ;
#7885=AXIS2_PLACEMENT_3D ( 'NONE', #7497, #4089, #3161 ) ;
#7897=ORIENTED_EDGE ( 'NONE', *, *, #6771, .F. ) ;
#7966=CARTESIAN_POINT ( 'NONE',  ( 1.424271237134740131, -4.556291390728484991, -5.579847667638274858E-16 ) ) ;
#7967=AXIS2_PLACEMENT_3D ( 'NONE', #6111, #12784, #6040 ) ;
#7993=EDGE_CURVE ( 'NONE', #8297, #11341, #1833, .T. ) ;
#8022=EDGE_LOOP ( 'NONE', ( #3100, #13074, #6702, #12220 ) ) ;
#8029=DIRECTION ( 'NONE',  ( 0.000000000000000000, 0.000000000000000000, 1.000000000000000000 ) ) ;
#8033=( LENGTH_UNIT ( ) NAMED_UNIT ( * ) SI_UNIT ( .MILLI., .METRE. ) );
#8039=ORIENTED_EDGE ( 'NONE', *, *, #1399, .T. ) ;
#8081=ADVANCED_FACE ( 'NONE', ( #9824 ), #6620, .T. ) ;
#8107=EDGE_CURVE ( 'NONE', #1904, #6772, #870, .T. ) ;
#8112=ORIENTED_EDGE ( 'NONE', *, *, #10137, .F. ) ;
#8113=FACE_OUTER_BOUND ( 'NONE', #8022, .T. ) ;
#8143=CARTESIAN_POINT ( 'NONE',  ( 0.9586399445693771781, -0.5149999999999964606, -0.8293189044373090457 ) ) ;
#8151=PRODUCT_DEFINITION ( 'UNKNOWN', '', #500, #10454 ) ;
#8153=CARTESIAN_POINT ( 'NONE',  ( 0.000000000000000000, 0.5149999999999917977, 2.350000000000001865 ) ) ;
#8160=ADVANCED_FACE ( 'NONE', ( #13150 ), #8267, .T. ) ;
#8177=EDGE_CURVE ( 'NONE', #1098, #5839, #7426, .T. ) ;
#8186=DIRECTION ( 'NONE',  ( 0.4461977533474923430, 3.124646727056501017E-15, -0.8949343913984144638 ) ) ;
#8211=VECTOR ( 'NONE', #5873, 1000.000000000000000 ) ;
#8215=DIRECTION ( 'NONE',  ( -1.000000000000000000, 0.000000000000000000, -0.000000000000000000 ) ) ;
#8247=( NAMED_UNIT ( * ) SI_UNIT ( $, .STERADIAN. ) SOLID_ANGLE_UNIT ( ) );
#8251=EDGE_CURVE ( 'NONE', #13211, #9987, #10835, .T. ) ;
#8267=TOROIDAL_SURFACE ( 'NONE', #11513, 4.300000000000001599, 0.4499999999999985678 ) ;
#8268=CARTESIAN_POINT ( 'NONE',  ( 1.424271237134740131, 5.698459981794101142E-16, -4.556291390728477886 ) ) ;
#8272=VECTOR ( 'NONE', #12159, 1000.000000000000114 ) ;
#8297=VERTEX_POINT ( 'NONE', #334 ) ;
#8321=CIRCLE ( 'NONE', #9263, 1.037871761867652065 ) ;
#8326=DIRECTION ( 'NONE',  ( 0.000000000000000000, 0.000000000000000000, 1.000000000000000000 ) ) ;
#8354=ORIENTED_EDGE ( 'NONE', *, *, #8701, .T. ) ;
#8368=VERTEX_POINT ( 'NONE', #3786 ) ;
#8373=STYLED_ITEM ( 'NONE', ( #13540 ), #6456 ) ;
#8377=VERTEX_POINT ( 'NONE', #1515 ) ;
#8381=DIRECTION ( 'NONE',  ( 0.000000000000000000, 0.000000000000000000, 1.000000000000000000 ) ) ;
#8406=CYLINDRICAL_SURFACE ( 'NONE', #2614, 2.500000000000000000 ) ;
#8408=FACE_OUTER_BOUND ( 'NONE', #12726, .T. ) ;
#8422=EDGE_LOOP ( 'NONE', ( #6890, #10633, #11320, #2722, #3898, #5433, #1619 ) ) ;
#8434=EDGE_CURVE ( 'NONE', #9602, #11786, #2504, .T. ) ;
#8436=DIRECTION ( 'NONE',  ( -0.000000000000000000, 0.000000000000000000, 1.000000000000000000 ) ) ;
#8449=EDGE_CURVE ( 'NONE', #4728, #8297, #12221, .T. ) ;
#8467=CARTESIAN_POINT ( 'NONE',  ( 0.3226060873438401089, 2.189154565102731098, 0.5149999999999992362 ) ) ;
#8479=ORIENTED_EDGE ( 'NONE', *, *, #12585, .F. ) ;
#8480=FACE_OUTER_BOUND ( 'NONE', #5144, .T. ) ;
#8505=CARTESIAN_POINT ( 'NONE',  ( 3.016506661494197328, 8.581769150706125103E-33, -7.007546303702493782E-17 ) ) ;
#8528=CARTESIAN_POINT ( 'NONE',  ( 2.740000000000000213, 0.5150000000000035660, -0.9838866223905657904 ) ) ;
#8562=ORIENTED_EDGE ( 'NONE', *, *, #10342, .T. ) ;
#8569=AXIS2_PLACEMENT_3D ( 'NONE', #3176, #1031, #3388 ) ;
#8577=VECTOR ( 'NONE', #5178, 1000.000000000000000 ) ;
#8589=AXIS2_PLACEMENT_3D ( 'NONE', #12392, #1358, #11523 ) ;
#8593=CIRCLE ( 'NONE', #10443, 7.983406227920510467 ) ;
#8596=CARTESIAN_POINT ( 'NONE',  ( 0.06760930072668806801, -4.837354856632045452E-15, 0.000000000000000000 ) ) ;
#8628=FACE_OUTER_BOUND ( 'NONE', #5941, .T. ) ;
#8631=CARTESIAN_POINT ( 'NONE',  ( 0.000000000000000000, -0.5149999999999909095, -2.349999999999999201 ) ) ;
#8660=CARTESIAN_POINT ( 'NONE',  ( 0.000000000000000000, 2.349999999999998312, -0.5150000000000000133 ) ) ;
#8669=DIRECTION ( 'NONE',  ( -0.000000000000000000, 0.000000000000000000, 1.000000000000000000 ) ) ;
#8700=PLANE ( 'NONE',  #3851 ) ;
#8701=EDGE_CURVE ( 'NONE', #246, #9196, #9353, .T. ) ;
#8733=ORIENTED_EDGE ( 'NONE', *, *, #3233, .F. ) ;
#8755=VERTEX_POINT ( 'NONE', #10434 ) ;
#8770=ORIENTED_EDGE ( 'NONE', *, *, #11830, .T. ) ;
#8780=CARTESIAN_POINT ( 'NONE',  ( 2.740000000000000213, 0.000000000000000000, 0.000000000000000000 ) ) ;
#8793=AXIS2_PLACEMENT_3D ( 'NONE', #13677, #3747, #9183 ) ;
#8800=CARTESIAN_POINT ( 'NONE',  ( 1.794155980045909482, 0.000000000000000000, 0.000000000000000000 ) ) ;
#8819=EDGE_CURVE ( 'NONE', #1387, #11692, #4787, .T. ) ;
#8823=FACE_OUTER_BOUND ( 'NONE', #9939, .T. ) ;
#8824=DIRECTION ( 'NONE',  ( 0.000000000000000000, 0.000000000000000000, 1.000000000000000000 ) ) ;
#8833=AXIS2_PLACEMENT_3D ( 'NONE', #221, #4683, #4754 ) ;
#8841=VERTEX_POINT ( 'NONE', #3190 ) ;
#8855=DIRECTION ( 'NONE',  ( -1.000000000000000000, -0.000000000000000000, -0.000000000000000000 ) ) ;
#8875=EDGE_CURVE ( 'NONE', #1387, #7393, #3443, .T. ) ;
#8880=CIRCLE ( 'NONE', #13492, 2.500000000000000000 ) ;
#8897=LINE ( 'NONE', #13173, #7165 ) ;
#8916=ORIENTED_EDGE ( 'NONE', *, *, #4615, .T. ) ;
#8920=CONICAL_SURFACE ( 'NONE', #551, 0.8509999999999999787, 0.06981317007976602096 ) ;
#8927=CARTESIAN_POINT ( 'NONE',  ( 2.740000000000000213, 0.000000000000000000, 0.000000000000000000 ) ) ;
#8932=CARTESIAN_POINT ( 'NONE',  ( 0.9586399445693778443, 0.8293189044373067143, -0.5150000000000000133 ) ) ;
#8936=DIRECTION ( 'NONE',  ( -1.000000000000000000, -0.000000000000000000, -0.000000000000000000 ) ) ;
#8940=CARTESIAN_POINT ( 'NONE',  ( 8.000000000000000000, -0.5149999999999999023, -1.857513327677604022E-15 ) ) ;
#8948=DIRECTION ( 'NONE',  ( -0.000000000000000000, 1.000000000000000000, 1.224646799147353207E-16 ) ) ;
#8981=VERTEX_POINT ( 'NONE', #12378 ) ;
#9003=DIRECTION ( 'NONE',  ( -1.000000000000000000, -0.000000000000000000, -0.000000000000000000 ) ) ;
#9007=B_SPLINE_CURVE_WITH_KNOTS ( 'NONE', 3,
 ( #2031, #2104, #7610, #3212 ),
 .UNSPECIFIED., .F., .F.,
 ( 4, 4 ),
 ( 0.004656695506220393486, 0.007337072593346777132 ),
 .UNSPECIFIED. ) ;
#9022=CARTESIAN_POINT ( 'NONE',  ( 8.000000000000000000, -0.5149999999999999023, -1.857513327677604022E-15 ) ) ;
#9040=ADVANCED_FACE ( 'NONE', ( #4844 ), #6932, .F. ) ;
#9044=AXIS2_PLACEMENT_3D ( 'NONE', #13537, #106, #12326 ) ;
#9089=AXIS2_PLACEMENT_3D ( 'NONE', #1474, #1405, #11150 ) ;
#9114=CARTESIAN_POINT ( 'NONE',  ( 2.740000000000000213, 0.000000000000000000, 0.000000000000000000 ) ) ;
#9119=PRODUCT_DEFINITION_SHAPE ( 'NONE', 'NONE',  #8151 ) ;
#9149=LINE ( 'NONE', #11980, #8577 ) ;
#9153=DIRECTION ( 'NONE',  ( 0.000000000000000000, 1.000000000000000000, 0.000000000000000000 ) ) ;
#9183=DIRECTION ( 'NONE',  ( 0.000000000000000000, -1.224646799147352714E-16, 1.000000000000000000 ) ) ;
#9188=VERTEX_POINT ( 'NONE', #957 ) ;
#9196=VERTEX_POINT ( 'NONE', #8528 ) ;
#9211=VERTEX_POINT ( 'NONE', #12877 ) ;
#9263=AXIS2_PLACEMENT_3D ( 'NONE', #5347, #5416, #13170 ) ;
#9264=DIRECTION ( 'NONE',  ( 0.000000000000000000, -1.000000000000000000, -3.491481338843133355E-15 ) ) ;
#9275=VECTOR ( 'NONE', #5486, 1000.000000000000000 ) ;
#9277=DIRECTION ( 'NONE',  ( 1.007709689656716938E-16, 1.153406566473941260E-16, -1.000000000000000000 ) ) ;
#9281=AXIS2_PLACEMENT_3D ( 'NONE', #13405, #314, #8029 ) ;
#9287=DIRECTION ( 'NONE',  ( -1.000000000000000000, -0.000000000000000000, -0.000000000000000000 ) ) ;
#9293=LINE ( 'NONE', #12620, #10840 ) ;
#9310=TOROIDAL_SURFACE ( 'NONE', #12788, 4.300000000000001599, 0.4499999999999985678 ) ;
#9332=EDGE_CURVE ( 'NONE', #1098, #8981, #10227, .T. ) ;
#9349=EDGE_CURVE ( 'NONE', #8755, #4266, #2580, .T. ) ;
#9353=LINE ( 'NONE', #3906, #5980 ) ;
#9369=EDGE_LOOP ( 'NONE', ( #98, #1572, #12209, #1932 ) ) ;
#9380=DIRECTION ( 'NONE',  ( -1.000000000000000000, 0.000000000000000000, -0.000000000000000000 ) ) ;
#9394=ORIENTED_EDGE ( 'NONE', *, *, #1129, .F. ) ;
#9399=( NAMED_UNIT ( * ) PLANE_ANGLE_UNIT ( ) SI_UNIT ( $, .RADIAN. ) );
#9408=ORIENTED_EDGE ( 'NONE', *, *, #7519, .T. ) ;
#9409=LINE ( 'NONE', #13822, #13430 ) ;
#9412=CIRCLE ( 'NONE', #1040, 1.037871761867652065 ) ;
#9418=DIRECTION ( 'NONE',  ( 0.000000000000000000, 0.000000000000000000, 1.000000000000000000 ) ) ;
#9430=AXIS2_PLACEMENT_3D ( 'NONE', #11326, #9003, #13494 ) ;
#9431=DIRECTION ( 'NONE',  ( -1.000000000000000000, -0.000000000000000000, -0.000000000000000000 ) ) ;
#9445=MECHANICAL_DESIGN_GEOMETRIC_PRESENTATION_REPRESENTATION('',(#10851),#6900);
#9456=DIRECTION ( 'NONE',  ( -0.000000000000000000, 0.000000000000000000, 1.000000000000000000 ) ) ;
#9468=ADVANCED_FACE ( 'NONE', ( #12506 ), #2644, .T. ) ;
#9490=EDGE_CURVE ( 'NONE', #2281, #5030, #11562, .T. ) ;
#9542=FACE_OUTER_BOUND ( 'NONE', #9993, .T. ) ;
#9559=ORIENTED_EDGE ( 'NONE', *, *, #2621, .T. ) ;
#9600=CARTESIAN_POINT ( 'NONE',  ( 1.794155980045911036, 0.000000000000000000, 4.749999999999999112 ) ) ;
#9602=VERTEX_POINT ( 'NONE', #3213 ) ;
#9610=ADVANCED_FACE ( 'NONE', ( #10548 ), #9310, .T. ) ;
#9637=DIRECTION ( 'NONE',  ( 0.000000000000000000, 0.000000000000000000, 1.000000000000000000 ) ) ;
#9665=CARTESIAN_POINT ( 'NONE',  ( 2.740000000000000213, 0.5149999999999965716, 0.9838866223910015529 ) ) ;
#9682=DIRECTION ( 'NONE',  ( -0.000000000000000000, 0.000000000000000000, 1.000000000000000000 ) ) ;
#9724=DIRECTION ( 'NONE',  ( -1.000000000000000000, -0.000000000000000000, -0.000000000000000000 ) ) ;
#9741=PLANE ( 'NONE',  #1720 ) ;
#9745=ORIENTED_EDGE ( 'NONE', *, *, #13389, .F. ) ;
#9747=ORIENTED_EDGE ( 'NONE', *, *, #5351, .T. ) ;
#9750=CARTESIAN_POINT ( 'NONE',  ( 0.06760930072668894231, -0.9010842325122929708, -0.5150000000000000133 ) ) ;
#9766=FACE_OUTER_BOUND ( 'NONE', #1344, .T. ) ;
#9781=B_SPLINE_CURVE_WITH_KNOTS ( 'NONE', 3,
 ( #10870, #11954, #10797, #11807 ),
 .UNSPECIFIED., .F., .F.,
 ( 4, 4 ),
 ( 0.004656695506220393486, 0.007337072593346776264 ),
 .UNSPECIFIED. ) ;
#9820=CARTESIAN_POINT ( 'NONE',  ( 1.424271237134740131, 0.000000000000000000, 0.000000000000000000 ) ) ;
#9824=FACE_OUTER_BOUND ( 'NONE', #14298, .T. ) ;
#9853=AXIS2_PLACEMENT_3D ( 'NONE', #6470, #12191, #11987 ) ;
#9866=VERTEX_POINT ( 'NONE', #7824 ) ;
#9876=ORIENTED_EDGE ( 'NONE', *, *, #1399, .F. ) ;
#9919=AXIS2_PLACEMENT_3D ( 'NONE', #6225, #5152, #9637 ) ;
#9922=ORIENTED_EDGE ( 'NONE', *, *, #8875, .F. ) ;
#9939=EDGE_LOOP ( 'NONE', ( #14083, #2579, #11935, #7044 ) ) ;
#9945=DIRECTION ( 'NONE',  ( -1.000000000000000000, -0.000000000000000000, -0.000000000000000000 ) ) ;
#9951=EDGE_LOOP ( 'NONE', ( #4180, #7435 ) ) ;
#9952=ORIENTED_EDGE ( 'NONE', *, *, #13309, .F. ) ;
#9960=LINE ( 'NONE', #6692, #5957 ) ;
#9979=DIRECTION ( 'NONE',  ( 0.000000000000000000, 0.000000000000000000, 1.000000000000000000 ) ) ;
#9980=DIRECTION ( 'NONE',  ( 0.000000000000000000, 0.000000000000000000, -1.000000000000000000 ) ) ;
#9985=PLANE ( 'NONE',  #669 ) ;
#9987=VERTEX_POINT ( 'NONE', #466 ) ;
#9993=EDGE_LOOP ( 'NONE', ( #13635, #10553, #2446, #875, #10765 ) ) ;
#10021=FACE_OUTER_BOUND ( 'NONE', #7746, .T. ) ;
#10026=CARTESIAN_POINT ( 'NONE',  ( 2.740000000000000213, 0.5150000000000035660, -0.9838866223905657904 ) ) ;
#10035=DIRECTION ( 'NONE',  ( 0.000000000000000000, -3.606821995490527259E-15, 1.000000000000000000 ) ) ;
#10060=FACE_OUTER_BOUND ( 'NONE', #14057, .T. ) ;
#10071=EDGE_LOOP ( 'NONE', ( #1639, #7594, #9394, #4016, #9952 ) ) ;
#10086=AXIS2_PLACEMENT_3D ( 'NONE', #3838, #2754, #4206 ) ;
#10087=VERTEX_POINT ( 'NONE', #11361 ) ;
#10089=ORIENTED_EDGE ( 'NONE', *, *, #1129, .T. ) ;
#10090=DIRECTION ( 'NONE',  ( 0.000000000000000000, 0.000000000000000000, 1.000000000000000000 ) ) ;
#10098=FACE_OUTER_BOUND ( 'NONE', #10724, .T. ) ;
#10107=ADVANCED_FACE ( 'NONE', ( #5770 ), #6075, .F. ) ;
#10124=EDGE_CURVE ( 'NONE', #4728, #5839, #3740, .T. ) ;
#10137=EDGE_CURVE ( 'NONE', #1103, #10087, #2610, .T. ) ;
#10156=DIRECTION ( 'NONE',  ( 1.000000000000000000, 0.000000000000000000, 0.000000000000000000 ) ) ;
#10165=PRODUCT ( 'pan head cross recess screw_iso_ISO 7045 - M5 x 25 - Z - 25N', 'pan head cross recess screw_iso_ISO 7045 - M5 x 25 - Z - 25N', '', ( #5961 ) ) ;
#10189=DIRECTION ( 'NONE',  ( -1.000000000000000000, -0.000000000000000000, -0.000000000000000000 ) ) ;
#10220=EDGE_CURVE ( 'NONE', #1514, #7747, #10951, .T. ) ;
#10227=CIRCLE ( 'NONE', #7445, 0.8509999999999999787 ) ;
#10239=ORIENTED_EDGE ( 'NONE', *, *, #7159, .F. ) ;
#10241=AXIS2_PLACEMENT_3D ( 'NONE', #1901, #4154, #7693 ) ;
#10267=CARTESIAN_POINT ( 'NONE',  ( 8.000000000000000000, 0.5150000000000000133, 1.798112889504231112E-15 ) ) ;
#10328=CARTESIAN_POINT ( 'NONE',  ( 1.424271237134740131, 0.000000000000000000, 0.000000000000000000 ) ) ;
#10342=EDGE_CURVE ( 'NONE', #9188, #8841, #937, .T. ) ;
#10359=AXIS2_PLACEMENT_3D ( 'NONE', #4362, #2102, #12917 ) ;
#10362=SURFACE_SIDE_STYLE ('',( #5936 ) ) ;
#10370=EDGE_CURVE ( 'NONE', #9196, #14235, #6424, .T. ) ;
#10389=EDGE_CURVE ( 'NONE', #9987, #6099, #7476, .T. ) ;
#10392=ADVANCED_FACE ( 'NONE', ( #9766 ), #10492, .F. ) ;
#10395=VERTEX_POINT ( 'NONE', #13022 ) ;
#10413=DIRECTION ( 'NONE',  ( 0.000000000000000000, 0.000000000000000000, 1.000000000000000000 ) ) ;
#10422=AXIS2_PLACEMENT_3D ( 'NONE', #11947, #11079, #12226 ) ;
#10423=DIRECTION ( 'NONE',  ( 0.000000000000000000, -1.000000000000000000, -3.491481338843133355E-15 ) ) ;
#10434=CARTESIAN_POINT ( 'NONE',  ( 0.06760930072668894231, 0.9010842325122760954, 0.5149999999999993472 ) ) ;
#10443=AXIS2_PLACEMENT_3D ( 'NONE', #10267, #2514, #4760 ) ;
#10452=CARTESIAN_POINT ( 'NONE',  ( 0.06760930072668806801, -4.837354856632045452E-15, 0.000000000000000000 ) ) ;
#10454=PRODUCT_DEFINITION_CONTEXT ( 'detailed design', #13313, 'design' ) ;
#10456=ADVANCED_FACE ( 'NONE', ( #6353 ), #4177, .T. ) ;
#10479=CARTESIAN_POINT ( 'NONE',  ( 0.3226060873438244547, -2.189154565102685801, 0.5149999999999992362 ) ) ;
#10482=ORIENTED_EDGE ( 'NONE', *, *, #8819, .F. ) ;
#10492=TOROIDAL_SURFACE ( 'NONE', #12580, 2.700000000000000178, 0.2000000000000000111 ) ;
#10503=DIRECTION ( 'NONE',  ( -0.000000000000000000, 0.000000000000000000, -1.000000000000000000 ) ) ;
#10508=CARTESIAN_POINT ( 'NONE',  ( 0.000000000000000000, 0.000000000000000000, 0.000000000000000000 ) ) ;
#10536=ORIENTED_EDGE ( 'NONE', *, *, #7519, .F. ) ;
#10548=FACE_OUTER_BOUND ( 'NONE', #4790, .T. ) ;
#10553=ORIENTED_EDGE ( 'NONE', *, *, #10220, .F. ) ;
#10559=ORIENTED_EDGE ( 'NONE', *, *, #8107, .F. ) ;
#10574=AXIS2_PLACEMENT_3D ( 'NONE', #2325, #10423, #378 ) ;
#10599=VECTOR ( 'NONE', #9153, 1000.000000000000000 ) ;
#10606=ORIENTED_EDGE ( 'NONE', *, *, #3580, .T. ) ;
#10620=AXIS2_PLACEMENT_3D ( 'NONE', #12365, #11072, #5625 ) ;
#10623=DIRECTION ( 'NONE',  ( -1.000000000000000000, -0.000000000000000000, -0.000000000000000000 ) ) ;
#10631=LINE ( 'NONE', #4971, #12244 ) ;
#10633=ORIENTED_EDGE ( 'NONE', *, *, #6816, .T. ) ;
#10646=ADVANCED_FACE ( 'NONE', ( #1022 ), #2135, .T. ) ;
#10660=EDGE_CURVE ( 'NONE', #11926, #5030, #8880, .T. ) ;
#10706=ORIENTED_EDGE ( 'NONE', *, *, #10660, .T. ) ;
#10709=COLOUR_RGB ( '',1.000000000000000000, 0.9490196078431372140, 0.9098039215686274384 ) ;
#10710=ORIENTED_EDGE ( 'NONE', *, *, #5055, .T. ) ;
#10711=CARTESIAN_POINT ( 'NONE',  ( 3.900000000000000799, 3.061616997868383141E-16, -2.500000000000000000 ) ) ;
#10724=EDGE_LOOP ( 'NONE', ( #4336, #12334, #13990, #2528, #4875 ) ) ;
#10725=ORIENTED_EDGE ( 'NONE', *, *, #12585, .T. ) ;
#10756=EDGE_CURVE ( 'NONE', #10395, #11926, #1915, .T. ) ;
#10765=ORIENTED_EDGE ( 'NONE', *, *, #10370, .T. ) ;
#10777=ORIENTED_EDGE ( 'NONE', *, *, #8449, .F. ) ;
#10797=CARTESIAN_POINT ( 'NONE',  ( 0.9586399445693630783, 0.5150000000000030109, -0.8293189044373061591 ) ) ;
#10801=VECTOR ( 'NONE', #1011, 1000.000000000000341 ) ;
#10810=CARTESIAN_POINT ( 'NONE',  ( -25.39999999999996305, 0.000000000000000000, 0.000000000000000000 ) ) ;
#10812=AXIS2_PLACEMENT_3D ( 'NONE', #11417, #5828, #3655 ) ;
#10825=VECTOR ( 'NONE', #10623, 1000.000000000000000 ) ;
#10830=DIRECTION ( 'NONE',  ( 0.4461977533474923430, 3.124646727056501411E-15, -0.8949343913984144638 ) ) ;
#10835=CIRCLE ( 'NONE', #1540, 7.983406227920510467 ) ;
#10840=VECTOR ( 'NONE', #11253, 1000.000000000000000 ) ;
#10851=STYLED_ITEM('',(#14417),#13134);
#10865=CARTESIAN_POINT ( 'NONE',  ( 28.70000000000000284, 0.000000000000000000, 2.500000000000000000 ) ) ;
#10870=CARTESIAN_POINT ( 'NONE',  ( 2.740000000000000213, 0.5150000000000024558, -0.6774776749089207462 ) ) ;
#10872=ORIENTED_EDGE ( 'NONE', *, *, #10756, .F. ) ;
#10882=ORIENTED_EDGE ( 'NONE', *, *, #3977, .T. ) ;
#10918=EDGE_LOOP ( 'NONE', ( #1058, #4773, #1916, #2238, #9747 ) ) ;
#10924=CARTESIAN_POINT ( 'NONE',  ( 2.740000000000000213, -0.6774776749089230776, 0.5149999999999995692 ) ) ;
#10951=CIRCLE ( 'NONE', #12558, 0.8509999999999999787 ) ;
#10956=B_SPLINE_CURVE_WITH_KNOTS ( 'NONE', 3,
 ( #1255, #8143, #13662, #12583 ),
 .UNSPECIFIED., .F., .F.,
 ( 4, 4 ),
 ( 0.001586480563516617188, 0.004268227385920363680 ),
 .UNSPECIFIED. ) ;
#10978=ORIENTED_EDGE ( 'NONE', *, *, #9349, .T. ) ;
#11030=UNCERTAINTY_MEASURE_WITH_UNIT (LENGTH_MEASURE( 1.000000000000000082E-05 ), #8033, 'distance_accuracy_value', 'NONE');
#11048=ORIENTED_EDGE ( 'NONE', *, *, #5991, .F. ) ;
#11072=DIRECTION ( 'NONE',  ( 0.4461977533473793778, 0.8949343913984707521, -1.884057886186824495E-16 ) ) ;
#11079=DIRECTION ( 'NONE',  ( -0.000000000000000000, 0.000000000000000000, 1.000000000000000000 ) ) ;
#11103=ADVANCED_FACE ( 'NONE', ( #8628 ), #3126, .T. ) ;
#11117=LINE ( 'NONE', #10026, #8211 ) ;
#11149=CARTESIAN_POINT ( 'NONE',  ( 28.70000000000000284, 3.061616997868383141E-16, -2.500000000000000000 ) ) ;
#11150=DIRECTION ( 'NONE',  ( 0.000000000000000000, 0.000000000000000000, 1.000000000000000000 ) ) ;
#11180=ORIENTED_EDGE ( 'NONE', *, *, #3862, .T. ) ;
#11184=CARTESIAN_POINT ( 'NONE',  ( 0.3226060873438262311, 0.5150000000000077849, -2.189154565102684025 ) ) ;
#11229=ORIENTED_EDGE ( 'NONE', *, *, #13389, .T. ) ;
#11253=DIRECTION ( 'NONE',  ( 0.000000000000000000, -2.105246936865057790E-16, 1.000000000000000000 ) ) ;
#11274=DIRECTION ( 'NONE',  ( 0.000000000000000000, 3.656775105596099119E-15, -1.000000000000000000 ) ) ;
#11293=VECTOR ( 'NONE', #12135, 1000.000000000000000 ) ;
#11297=AXIS2_PLACEMENT_3D ( 'NONE', #10452, #407, #3636 ) ;
#11302=CIRCLE ( 'NONE', #11754, 0.8509999999999999787 ) ;
#11309=ORIENTED_EDGE ( 'NONE', *, *, #3977, .F. ) ;
#11320=ORIENTED_EDGE ( 'NONE', *, *, #10220, .T. ) ;
#11326=CARTESIAN_POINT ( 'NONE',  ( 2.740000000000000213, 0.000000000000000000, 0.000000000000000000 ) ) ;
#11341=VERTEX_POINT ( 'NONE', #382 ) ;
#11361=CARTESIAN_POINT ( 'NONE',  ( 0.06760930072668894231, 0.9010842325122832008, -0.5150000000000000133 ) ) ;
#11362=VERTEX_POINT ( 'NONE', #12597 ) ;
#11366=ADVANCED_FACE ( 'NONE', ( #458 ), #13903, .F. ) ;
#11382=EDGE_CURVE ( 'NONE', #8368, #12612, #9781, .T. ) ;
#11391=ORIENTED_EDGE ( 'NONE', *, *, #9349, .F. ) ;
#11392=EDGE_LOOP ( 'NONE', ( #3492, #1598, #7829, #14273, #5814, #11803, #14112, #5942, #13623, #11773, #8112, #809, #6386 ) ) ;
#11409=DIRECTION ( 'NONE',  ( -1.000000000000000000, -0.000000000000000000, -0.000000000000000000 ) ) ;
#11417=CARTESIAN_POINT ( 'NONE',  ( 8.000000000000000000, -4.837354856632045452E-15, 0.000000000000000000 ) ) ;
#11453=( LENGTH_UNIT ( ) NAMED_UNIT ( * ) SI_UNIT ( .MILLI., .METRE. ) );
#11513=AXIS2_PLACEMENT_3D ( 'NONE', #8800, #4241, #3160 ) ;
#11523=DIRECTION ( 'NONE',  ( 0.000000000000000000, 0.000000000000000000, 1.000000000000000000 ) ) ;
#11551=ORIENTED_EDGE ( 'NONE', *, *, #62, .T. ) ;
#11562=LINE ( 'NONE', #510, #12088 ) ;
#11580=FACE_OUTER_BOUND ( 'NONE', #10918, .T. ) ;
#11585=SPHERICAL_SURFACE ( 'NONE', #12976, 8.000000000000000000 ) ;
#11590=CARTESIAN_POINT ( 'NONE',  ( 28.70000000000000284, 0.000000000000000000, 0.000000000000000000 ) ) ;
#11600=VERTEX_POINT ( 'NONE', #11149 ) ;
#11612=ORIENTED_EDGE ( 'NONE', *, *, #4277, .T. ) ;
#11644=ORIENTED_EDGE ( 'NONE', *, *, #9490, .F. ) ;
#11654=DIRECTION ( 'NONE',  ( 1.007709689656716938E-16, 1.000000000000000000, 3.606821995490528048E-15 ) ) ;
#11675=DIRECTION ( 'NONE',  ( 0.000000000000000000, 0.000000000000000000, 1.000000000000000000 ) ) ;
#11678=FACE_OUTER_BOUND ( 'NONE', #12808, .T. ) ;
#11692=VERTEX_POINT ( 'NONE', #3738 ) ;
#11748=VECTOR ( 'NONE', #1905, 1000.000000000000341 ) ;
#11753=DIRECTION ( 'NONE',  ( -0.8949343913984144638, 0.000000000000000000, -0.4461977533474923430 ) ) ;
#11754=AXIS2_PLACEMENT_3D ( 'NONE', #3578, #11409, #13358 ) ;
#11773=ORIENTED_EDGE ( 'NONE', *, *, #13931, .F. ) ;
#11786=VERTEX_POINT ( 'NONE', #1699 ) ;
#11803=ORIENTED_EDGE ( 'NONE', *, *, #10389, .F. ) ;
#11807=CARTESIAN_POINT ( 'NONE',  ( 0.06760930072668812352, 0.5150000000000032330, -0.9010842325122888630 ) ) ;
#11830=EDGE_CURVE ( 'NONE', #12612, #246, #8593, .T. ) ;
#11853=ORIENTED_EDGE ( 'NONE', *, *, #6816, .F. ) ;
#11874=LINE ( 'NONE', #4184, #12505 ) ;
#11879=ORIENTED_EDGE ( 'NONE', *, *, #12593, .T. ) ;
#11883=DIRECTION ( 'NONE',  ( -1.000000000000000000, -0.000000000000000000, -0.000000000000000000 ) ) ;
#11903=ORIENTED_EDGE ( 'NONE', *, *, #4277, .F. ) ;
#11926=VERTEX_POINT ( 'NONE', #10711 ) ;
#11935=ORIENTED_EDGE ( 'NONE', *, *, #1177, .T. ) ;
#11940=CARTESIAN_POINT ( 'NONE',  ( 1.849560077140108172, -0.7556913915602447851, 0.5149999999999994582 ) ) ;
#11947=CARTESIAN_POINT ( 'NONE',  ( 8.000000000000000000, -4.837354856632045452E-15, 0.000000000000000000 ) ) ;
#11951=AXIS2_PLACEMENT_3D ( 'NONE', #4867, #9287, #7169 ) ;
#11954=CARTESIAN_POINT ( 'NONE',  ( 1.849560077140107284, 0.5150000000000026779, -0.7556913915602427867 ) ) ;
#11957=AXIS2_PLACEMENT_3D ( 'NONE', #12935, #14156, #4238 ) ;
#11980=CARTESIAN_POINT ( 'NONE',  ( -25.39999999999996305, 5.817072295949926440E-16, -4.749999999999999112 ) ) ;
#11987=DIRECTION ( 'NONE',  ( 0.000000000000000000, 1.000000000000000000, 1.224646799147353207E-16 ) ) ;
#11995=LINE ( 'NONE', #8505, #10801 ) ;
#12020=CARTESIAN_POINT ( 'NONE',  ( 2.740000000000000213, 0.9838866223910003317, 0.5149999999999999023 ) ) ;
#12038=EDGE_CURVE ( 'NONE', #5337, #8377, #1024, .T. ) ;
#12067=CIRCLE ( 'NONE', #9044, 7.864440107515625833 ) ;
#12088=VECTOR ( 'NONE', #13734, 1000.000000000000000 ) ;
#12135=DIRECTION ( 'NONE',  ( 0.000000000000000000, -3.491481338843133355E-15, 1.000000000000000000 ) ) ;
#12141=EDGE_CURVE ( 'NONE', #1896, #13924, #13578, .T. ) ;
#12159=DIRECTION ( 'NONE',  ( 0.8949343913984143528, -1.699539276894113739E-15, 0.4461977533474921764 ) ) ;
#12181=DIRECTION ( 'NONE',  ( 0.000000000000000000, 0.000000000000000000, 1.000000000000000000 ) ) ;
#12191=DIRECTION ( 'NONE',  ( 0.000000000000000000, 1.224646799147353207E-16, -1.000000000000000000 ) ) ;
#12209=ORIENTED_EDGE ( 'NONE', *, *, #2279, .F. ) ;
#12213=CIRCLE ( 'NONE', #11297, 1.037871761867652065 ) ;
#12214=ADVANCED_FACE ( 'NONE', ( #13794 ), #12498, .T. ) ;
#12220=ORIENTED_EDGE ( 'NONE', *, *, #10124, .F. ) ;
#12221=CIRCLE ( 'NONE', #6196, 7.864440107515624945 ) ;
#12226=DIRECTION ( 'NONE',  ( 1.000000000000000000, 0.000000000000000000, 0.000000000000000000 ) ) ;
#12244=VECTOR ( 'NONE', #661, 1000.000000000000000 ) ;
#12251=ORIENTED_EDGE ( 'NONE', *, *, #12038, .F. ) ;
#12265=ORIENTED_EDGE ( 'NONE', *, *, #2870, .T. ) ;
#12270=CIRCLE ( 'NONE', #8793, 0.4499999999999985678 ) ;
#12282=CARTESIAN_POINT ( 'NONE',  ( 0.000000000000000000, -2.349999999999999201, -0.5150000000000000133 ) ) ;
#12297=CONICAL_SURFACE ( 'NONE', #9281, 3077.683537175319998, 1.256637061435923686 ) ;
#12322=ORIENTED_EDGE ( 'NONE', *, *, #10137, .T. ) ;
#12326=DIRECTION ( 'NONE',  ( -0.8949343913984706411, 0.4461977533473793223, 0.000000000000000000 ) ) ;
#12329=AXIS2_PLACEMENT_3D ( 'NONE', #4545, #13597, #6929 ) ;
#12334=ORIENTED_EDGE ( 'NONE', *, *, #12675, .F. ) ;
#12357=EDGE_CURVE ( 'NONE', #11600, #11926, #1829, .T. ) ;
#12364=CARTESIAN_POINT ( 'NONE',  ( 2.740000000000000213, 0.9838866223910003317, 0.5149999999999999023 ) ) ;
#12365=CARTESIAN_POINT ( 'NONE',  ( 7.345657149124971141, -1.312408941149200814, 2.762944903268657774E-16 ) ) ;
#12378=CARTESIAN_POINT ( 'NONE',  ( 2.740000000000000213, 0.6774776749089228556, 0.5149999999999997913 ) ) ;
#12381=CIRCLE ( 'NONE', #7517, 4.750000000000000000 ) ;
#12382=ORIENTED_EDGE ( 'NONE', *, *, #4615, .F. ) ;
#12384=ORIENTED_EDGE ( 'NONE', *, *, #517, .F. ) ;
#12392=CARTESIAN_POINT ( 'NONE',  ( 2.740000000000000213, 0.000000000000000000, 0.000000000000000000 ) ) ;
#12399=ORIENTED_EDGE ( 'NONE', *, *, #3152, .T. ) ;
#12428=EDGE_CURVE ( 'NONE', #7102, #5706, #14008, .T. ) ;
#12486=ORIENTED_EDGE ( 'NONE', *, *, #10756, .T. ) ;
#12498=SPHERICAL_SURFACE ( 'NONE', #10812, 8.000000000000000000 ) ;
#12505=VECTOR ( 'NONE', #6358, 1000.000000000000114 ) ;
#12506=FACE_OUTER_BOUND ( 'NONE', #3917, .T. ) ;
#12548=ORIENTED_EDGE ( 'NONE', *, *, #62, .F. ) ;
#12549=PLANE ( 'NONE',  #6611 ) ;
#12558=AXIS2_PLACEMENT_3D ( 'NONE', #4911, #5059, #10413 ) ;
#12568=VECTOR ( 'NONE', #2515, 1000.000000000000114 ) ;
#12570=CARTESIAN_POINT ( 'NONE',  ( 0.000000000000000000, 2.350000000000000089, 0.5149999999999996803 ) ) ;
#12580=AXIS2_PLACEMENT_3D ( 'NONE', #7506, #3315, #3169 ) ;
#12583=CARTESIAN_POINT ( 'NONE',  ( 2.740000000000000213, -0.5149999999999973488, -0.6774776749089248540 ) ) ;
#12584=CARTESIAN_POINT ( 'NONE',  ( 2.740000000000000213, 0.9838866223910001096, 0.5149999999999999023 ) ) ;
#12585=EDGE_CURVE ( 'NONE', #232, #1387, #9960, .T. ) ;
#12593=EDGE_CURVE ( 'NONE', #1600, #7393, #2480, .T. ) ;
#12596=FACE_OUTER_BOUND ( 'NONE', #11392, .T. ) ;
#12597=CARTESIAN_POINT ( 'NONE',  ( 0.06760930072668799862, 0.5149999999999969047, 0.9010842325122926377 ) ) ;
#12612=VERTEX_POINT ( 'NONE', #2337 ) ;
#12620=CARTESIAN_POINT ( 'NONE',  ( 2.740000000000000213, -0.9838866223905674557, -0.5150000000000000133 ) ) ;
#12625=CYLINDRICAL_SURFACE ( 'NONE', #7629, 4.749999999999999112 ) ;
#12645=ORIENTED_EDGE ( 'NONE', *, *, #2447, .T. ) ;
#12647=CIRCLE ( 'NONE', #5469, 2.500000000000000000 ) ;
#12675=EDGE_CURVE ( 'NONE', #6378, #8377, #9293, .T. ) ;
#12685=ADVANCED_FACE ( 'NONE', ( #7107 ), #1305, .F. ) ;
#12693=CARTESIAN_POINT ( 'NONE',  ( 2.740000000000000213, 0.6774776749089228556, 0.5149999999999997913 ) ) ;
#12723=DIRECTION ( 'NONE',  ( -0.000000000000000000, 0.000000000000000000, 1.000000000000000000 ) ) ;
#12726=EDGE_LOOP ( 'NONE', ( #379, #6792, #10978, #10089 ) ) ;
#12734=AXIS2_PLACEMENT_3D ( 'NONE', #6138, #1630, #6071 ) ;
#12753=AXIS2_PLACEMENT_3D ( 'NONE', #6879, #9277, #1432 ) ;
#12784=DIRECTION ( 'NONE',  ( -1.000000000000000000, -0.000000000000000000, -0.000000000000000000 ) ) ;
#12788=AXIS2_PLACEMENT_3D ( 'NONE', #6535, #12799, #14214 ) ;
#12799=DIRECTION ( 'NONE',  ( -1.000000000000000000, -0.000000000000000000, -0.000000000000000000 ) ) ;
#12805=ORIENTED_EDGE ( 'NONE', *, *, #3233, .T. ) ;
#12808=EDGE_LOOP ( 'NONE', ( #9408, #5564, #10706, #11644 ) ) ;
#12834=CARTESIAN_POINT ( 'NONE',  ( -25.39999999999996305, 0.000000000000000000, 0.000000000000000000 ) ) ;
#12865=ORIENTED_EDGE ( 'NONE', *, *, #7159, .T. ) ;
#12876=ADVANCED_FACE ( 'NONE', ( #8408 ), #12911, .T. ) ;
#12877=CARTESIAN_POINT ( 'NONE',  ( 2.740000000000000213, -0.6774776749089226335, -0.5150000000000000133 ) ) ;
#12881=PLANE ( 'NONE',  #12734 ) ;
#12894=VECTOR ( 'NONE', #5682, 1000.000000000000114 ) ;
#12896=DIRECTION ( 'NONE',  ( 0.000000000000000000, 0.000000000000000000, -1.000000000000000000 ) ) ;
#12911=PLANE ( 'NONE',  #5293 ) ;
#12917=DIRECTION ( 'NONE',  ( 0.8949343913984144638, 0.4461977533474923430, 0.000000000000000000 ) ) ;
#12931=CIRCLE ( 'NONE', #10620, 7.864440107515625833 ) ;
#12935=CARTESIAN_POINT ( 'NONE',  ( 7.345657149124338758, 1.312408941150044583, 0.000000000000000000 ) ) ;
#12962=ADVANCED_FACE ( 'NONE', ( #10060 ), #3465, .T. ) ;
#12967=CARTESIAN_POINT ( 'NONE',  ( 0.06760930072668813740, -0.5150000000000026779, 0.9010842325122891960 ) ) ;
#12976=AXIS2_PLACEMENT_3D ( 'NONE', #5923, #10503, #5073 ) ;
#13001=DIRECTION ( 'NONE',  ( 0.8949343913984143528, -1.557891129246500526E-15, 0.4461977533474922875 ) ) ;
#13022=CARTESIAN_POINT ( 'NONE',  ( 3.700000000000000178, 3.306546357697853733E-16, -2.700000000000000178 ) ) ;
#13071=EDGE_CURVE ( 'NONE', #13211, #14235, #4213, .T. ) ;
#13074=ORIENTED_EDGE ( 'NONE', *, *, #13487, .T. ) ;
#13092=CARTESIAN_POINT ( 'NONE',  ( 2.740000000000000213, 0.000000000000000000, 0.000000000000000000 ) ) ;
#13120=DIRECTION ( 'NONE',  ( 1.007709689656716815E-16, 1.153406566473941260E-16, -1.000000000000000000 ) ) ;
#13129=CARTESIAN_POINT ( 'NONE',  ( 1.424271237134740131, 0.000000000000000000, 0.000000000000000000 ) ) ;
#13134=MANIFOLD_SOLID_BREP ( 'RecessCore', #3589 ) ;
#13150=FACE_OUTER_BOUND ( 'NONE', #1272, .T. ) ;
#13159=VECTOR ( 'NONE', #11274, 1000.000000000000000 ) ;
#13162=CARTESIAN_POINT ( 'NONE',  ( 28.70000000000000284, 2.500000000000000000, 0.000000000000000000 ) ) ;
#13170=DIRECTION ( 'NONE',  ( 0.000000000000000000, 0.000000000000000000, -1.000000000000000000 ) ) ;
#13173=CARTESIAN_POINT ( 'NONE',  ( 2.740000000000000213, 0.9838866223910003317, 0.5149999999999999023 ) ) ;
#13211=VERTEX_POINT ( 'NONE', #883 ) ;
#13234=DIRECTION ( 'NONE',  ( 0.000000000000000000, 0.000000000000000000, -1.000000000000000000 ) ) ;
#13246=CARTESIAN_POINT ( 'NONE',  ( 0.000000000000000000, -0.5149999999999909095, -2.349999999999999201 ) ) ;
#13252=CARTESIAN_POINT ( 'NONE',  ( 0.000000000000000000, -0.5149999999999909095, -2.350000000000000977 ) ) ;
#13281=FACE_OUTER_BOUND ( 'NONE', #7504, .T. ) ;
#13307=CARTESIAN_POINT ( 'NONE',  ( 3.900000000000000799, 0.000000000000000000, 2.500000000000000000 ) ) ;
#13309=EDGE_CURVE ( 'NONE', #1103, #6825, #12931, .T. ) ;
#13313=APPLICATION_CONTEXT ( 'automotive_design' ) ;
#13328=EDGE_CURVE ( 'NONE', #11341, #9866, #13369, .T. ) ;
#13336=CARTESIAN_POINT ( 'NONE',  ( 2.740000000000000213, 0.000000000000000000, 0.000000000000000000 ) ) ;
#13343=CARTESIAN_POINT ( 'NONE',  ( 2.740000000000000213, 0.6774776749089226335, -0.5150000000000000133 ) ) ;
#13353=DIRECTION ( 'NONE',  ( 0.000000000000000000, -3.612465276695121047E-15, 1.000000000000000000 ) ) ;
#13358=DIRECTION ( 'NONE',  ( 0.000000000000000000, 0.000000000000000000, 1.000000000000000000 ) ) ;
#13369=LINE ( 'NONE', #6571, #13159 ) ;
#13389=EDGE_CURVE ( 'NONE', #7620, #8297, #5063, .T. ) ;
#13405=CARTESIAN_POINT ( 'NONE',  ( -996.9834933385058093, 0.000000000000000000, 0.000000000000000000 ) ) ;
#13418=ORIENTED_EDGE ( 'NONE', *, *, #13071, .T. ) ;
#13426=PLANE ( 'NONE',  #13889 ) ;
#13430=VECTOR ( 'NONE', #5356, 1000.000000000000114 ) ;
#13462=EDGE_LOOP ( 'NONE', ( #11853, #6770, #4313, #7741, #10606, #9559, #4397 ) ) ;
#13487=EDGE_CURVE ( 'NONE', #11362, #1098, #1093, .T. ) ;
#13492=AXIS2_PLACEMENT_3D ( 'NONE', #6705, #4530, #7850 ) ;
#13494=DIRECTION ( 'NONE',  ( 0.000000000000000000, 0.000000000000000000, 1.000000000000000000 ) ) ;
#13537=CARTESIAN_POINT ( 'NONE',  ( 7.345657149124971141, -1.312408941149200814, 2.762944903268657774E-16 ) ) ;
#13540=PRESENTATION_STYLE_ASSIGNMENT (( #4862 ) ) ;
#13547=CIRCLE ( 'NONE', #11957, 7.864440107515430434 ) ;
#13578=CIRCLE ( 'NONE', #587, 4.556291390728477886 ) ;
#13597=DIRECTION ( 'NONE',  ( -0.000000000000000000, 0.000000000000000000, 1.000000000000000000 ) ) ;
#13602=DIRECTION ( 'NONE',  ( 0.4461977533473793778, -2.936240938438015166E-15, 0.8949343913984707521 ) ) ;
#13623=ORIENTED_EDGE ( 'NONE', *, *, #11830, .F. ) ;
#13635=ORIENTED_EDGE ( 'NONE', *, *, #1177, .F. ) ;
#13638=CARTESIAN_POINT ( 'NONE',  ( 3.700000000000000178, 0.000000000000000000, 2.700000000000000178 ) ) ;
#13662=CARTESIAN_POINT ( 'NONE',  ( 1.849560077140141701, -0.5149999999999969047, -0.7556913915602436749 ) ) ;
#13673=( LENGTH_UNIT ( ) NAMED_UNIT ( * ) SI_UNIT ( .MILLI., .METRE. ) );
#13677=CARTESIAN_POINT ( 'NONE',  ( 1.794155980045909482, 5.265981236333621429E-16, -4.300000000000001599 ) ) ;
#13690=FACE_OUTER_BOUND ( 'NONE', #9369, .T. ) ;
#13705=EDGE_LOOP ( 'NONE', ( #5860, #11879, #10882, #7143, #12399, #11391, #10239, #11048, #4843, #9745, #1059, #6181, #175 ) ) ;
#13706=CARTESIAN_POINT ( 'NONE',  ( 3.016506661494197328, 7.007546303702493782E-17, 0.000000000000000000 ) ) ;
#13734=DIRECTION ( 'NONE',  ( -1.000000000000000000, -0.000000000000000000, -0.000000000000000000 ) ) ;
#13794=FACE_OUTER_BOUND ( 'NONE', #13705, .T. ) ;
#13798=DIRECTION ( 'NONE',  ( 0.000000000000000000, -3.612465276695121047E-15, 1.000000000000000000 ) ) ;
#13802=CARTESIAN_POINT ( 'NONE',  ( 2.740000000000000213, 0.9838866223910001096, -0.5150000000000001243 ) ) ;
#13812=DIRECTION ( 'NONE',  ( -0.8949343913984706411, -1.557891129246106096E-15, 0.4461977533473793223 ) ) ;
#13822=CARTESIAN_POINT ( 'NONE',  ( 0.000000000000000000, -2.349999999999999201, -0.5150000000000000133 ) ) ;
#13867=AXIS2_PLACEMENT_3D ( 'NONE', #8927, #4574, #4710 ) ;
#13884=CIRCLE ( 'NONE', #8569, 4.750000000000000000 ) ;
#13889=AXIS2_PLACEMENT_3D ( 'NONE', #12282, #131, #3441 ) ;
#13897=AXIS2_PLACEMENT_3D ( 'NONE', #2748, #688, #12896 ) ;
#13903=CONICAL_SURFACE ( 'NONE', #3272, 3077.683537175319998, 1.256637061435923686 ) ;
#13910=DIRECTION ( 'NONE',  ( 1.000000000000000000, 0.000000000000000000, 0.000000000000000000 ) ) ;
#13920=ORIENTED_EDGE ( 'NONE', *, *, #339, .T. ) ;
#13924=VERTEX_POINT ( 'NONE', #8268 ) ;
#13931=EDGE_CURVE ( 'NONE', #10087, #12612, #12213, .T. ) ;
#13978=DIRECTION ( 'NONE',  ( 0.000000000000000000, 0.000000000000000000, -1.000000000000000000 ) ) ;
#13990=ORIENTED_EDGE ( 'NONE', *, *, #972, .F. ) ;
#14003=CIRCLE ( 'NONE', #7967, 2.500000000000000000 ) ;
#14005=FACE_BOUND ( 'NONE', #9951, .T. ) ;
#14008=LINE ( 'NONE', #5039, #11748 ) ;
#14039=AXIS2_PLACEMENT_3D ( 'NONE', #10508, #9418, #5077 ) ;
#14040=ORIENTED_EDGE ( 'NONE', *, *, #4726, .F. ) ;
#14057=EDGE_LOOP ( 'NONE', ( #2190, #4064, #11229, #4838 ) ) ;
#14083=ORIENTED_EDGE ( 'NONE', *, *, #8251, .T. ) ;
#14112=ORIENTED_EDGE ( 'NONE', *, *, #8251, .F. ) ;
#14127=DIRECTION ( 'NONE',  ( 0.000000000000000000, 0.000000000000000000, 1.000000000000000000 ) ) ;
#14152=EDGE_LOOP ( 'NONE', ( #10872, #4153, #12805, #3059 ) ) ;
#14156=DIRECTION ( 'NONE',  ( 0.4461977533474923430, -0.8949343913984144638, 0.000000000000000000 ) ) ;
#14170=CIRCLE ( 'NONE', #10241, 4.749999999999999112 ) ;
#14171=DIRECTION ( 'NONE',  ( -1.000000000000000000, -0.000000000000000000, -0.000000000000000000 ) ) ;
#14210=ORIENTED_EDGE ( 'NONE', *, *, #5198, .F. ) ;
#14214=DIRECTION ( 'NONE',  ( 0.000000000000000000, 0.000000000000000000, 1.000000000000000000 ) ) ;
#14216=DIRECTION ( 'NONE',  ( 0.000000000000000000, 0.000000000000000000, 1.000000000000000000 ) ) ;
#14235=VERTEX_POINT ( 'NONE', #914 ) ;
#14240=CARTESIAN_POINT ( 'NONE',  ( 1.424271237134740131, 0.000000000000000000, 0.000000000000000000 ) ) ;
#14242=CIRCLE ( 'NONE', #9853, 8.000000000000000000 ) ;
#14245=DIRECTION ( 'NONE',  ( 1.007709689656716938E-16, 1.153406566473941260E-16, -1.000000000000000000 ) ) ;
#14270=CARTESIAN_POINT ( 'NONE',  ( 1.424271237134740131, 4.556291390728479662, 0.000000000000000000 ) ) ;
#14273=ORIENTED_EDGE ( 'NONE', *, *, #8434, .T. ) ;
#14283=DIRECTION ( 'NONE',  ( 0.000000000000000000, 0.000000000000000000, 1.000000000000000000 ) ) ;
#14298=EDGE_LOOP ( 'NONE', ( #12322, #2132, #726, #7553 ) ) ;
#14301=CARTESIAN_POINT ( 'NONE',  ( 0.9586399445693771781, -0.8293189044373066032, -0.5150000000000000133 ) ) ;
#14411=COLOUR_RGB('Black',0.12,0.14,0.17);
#14412=FILL_AREA_STYLE_COLOUR('',#14411);
#14413=FILL_AREA_STYLE('',(#14412));
#14414=SURFACE_STYLE_FILL_AREA(#14413);
#14415=SURFACE_SIDE_STYLE('',(#14414));
#14416=SURFACE_STYLE_USAGE(.BOTH.,#14415);
#14417=PRESENTATION_STYLE_ASSIGNMENT((#14416));
ENDSEC;
END-ISO-10303-21;
